ISO-10303-21;
HEADER;
/* Generated by software containing ST-Developer
 * from STEP Tools, Inc. (www.steptools.com) 
 */

FILE_DESCRIPTION(
/* description */ (''),
/* implementation_level */ '2;1');

FILE_NAME(
/* name */ '11_Block_Hold-Down_Spring_3x33x24.5.step',
/* time_stamp */ '2026-10-23T00:52:27+05:00',
/* author */ (''),
/* organization */ (''),
/* preprocessor_version */ 'ST-DEVELOPER v20.2',
/* originating_system */ 'Autodesk Translation Framework v15.15.0.0',
/* authorisation */ '');

FILE_SCHEMA (('AUTOMOTIVE_DESIGN { 1 0 10303 214 3 1 1 }'));
ENDSEC;

DATA;
#10=MECHANICAL_DESIGN_GEOMETRIC_PRESENTATION_REPRESENTATION('',(#1551),#59204);
#317=B_SPLINE_SURFACE_WITH_KNOTS('',3,3,((#31275,#31276,#31277,#31278,#31279,
#31280,#31281,#31282,#31283,#31284,#31285,#31286,#31287,#31288,#31289,#31290,
#31291,#31292,#31293,#31294,#31295,#31296,#31297,#31298,#31299,#31300,#31301,
#31302,#31303,#31304,#31305,#31306,#31307,#31308,#31309,#31310,#31311,#31312,
#31313,#31314,#31315,#31316,#31317,#31318,#31319,#31320,#31321,#31322,#31323,
#31324,#31325,#31326,#31327,#31328,#31329,#31330,#31331,#31332,#31333,#31334,
#31335,#31336,#31337,#31338,#31339,#31340,#31341,#31342,#31343,#31344,#31345,
#31346,#31347,#31348,#31349,#31350,#31351,#31352,#31353,#31354,#31355,#31356,
#31357),(#31358,#31359,#31360,#31361,#31362,#31363,#31364,#31365,#31366,
#31367,#31368,#31369,#31370,#31371,#31372,#31373,#31374,#31375,#31376,#31377,
#31378,#31379,#31380,#31381,#31382,#31383,#31384,#31385,#31386,#31387,#31388,
#31389,#31390,#31391,#31392,#31393,#31394,#31395,#31396,#31397,#31398,#31399,
#31400,#31401,#31402,#31403,#31404,#31405,#31406,#31407,#31408,#31409,#31410,
#31411,#31412,#31413,#31414,#31415,#31416,#31417,#31418,#31419,#31420,#31421,
#31422,#31423,#31424,#31425,#31426,#31427,#31428,#31429,#31430,#31431,#31432,
#31433,#31434,#31435,#31436,#31437,#31438,#31439,#31440),(#31441,#31442,
#31443,#31444,#31445,#31446,#31447,#31448,#31449,#31450,#31451,#31452,#31453,
#31454,#31455,#31456,#31457,#31458,#31459,#31460,#31461,#31462,#31463,#31464,
#31465,#31466,#31467,#31468,#31469,#31470,#31471,#31472,#31473,#31474,#31475,
#31476,#31477,#31478,#31479,#31480,#31481,#31482,#31483,#31484,#31485,#31486,
#31487,#31488,#31489,#31490,#31491,#31492,#31493,#31494,#31495,#31496,#31497,
#31498,#31499,#31500,#31501,#31502,#31503,#31504,#31505,#31506,#31507,#31508,
#31509,#31510,#31511,#31512,#31513,#31514,#31515,#31516,#31517,#31518,#31519,
#31520,#31521,#31522,#31523),(#31524,#31525,#31526,#31527,#31528,#31529,
#31530,#31531,#31532,#31533,#31534,#31535,#31536,#31537,#31538,#31539,#31540,
#31541,#31542,#31543,#31544,#31545,#31546,#31547,#31548,#31549,#31550,#31551,
#31552,#31553,#31554,#31555,#31556,#31557,#31558,#31559,#31560,#31561,#31562,
#31563,#31564,#31565,#31566,#31567,#31568,#31569,#31570,#31571,#31572,#31573,
#31574,#31575,#31576,#31577,#31578,#31579,#31580,#31581,#31582,#31583,#31584,
#31585,#31586,#31587,#31588,#31589,#31590,#31591,#31592,#31593,#31594,#31595,
#31596,#31597,#31598,#31599,#31600,#31601,#31602,#31603,#31604,#31605,#31606),
(#31607,#31608,#31609,#31610,#31611,#31612,#31613,#31614,#31615,#31616,
#31617,#31618,#31619,#31620,#31621,#31622,#31623,#31624,#31625,#31626,#31627,
#31628,#31629,#31630,#31631,#31632,#31633,#31634,#31635,#31636,#31637,#31638,
#31639,#31640,#31641,#31642,#31643,#31644,#31645,#31646,#31647,#31648,#31649,
#31650,#31651,#31652,#31653,#31654,#31655,#31656,#31657,#31658,#31659,#31660,
#31661,#31662,#31663,#31664,#31665,#31666,#31667,#31668,#31669,#31670,#31671,
#31672,#31673,#31674,#31675,#31676,#31677,#31678,#31679,#31680,#31681,#31682,
#31683,#31684,#31685,#31686,#31687,#31688,#31689),(#31690,#31691,#31692,
#31693,#31694,#31695,#31696,#31697,#31698,#31699,#31700,#31701,#31702,#31703,
#31704,#31705,#31706,#31707,#31708,#31709,#31710,#31711,#31712,#31713,#31714,
#31715,#31716,#31717,#31718,#31719,#31720,#31721,#31722,#31723,#31724,#31725,
#31726,#31727,#31728,#31729,#31730,#31731,#31732,#31733,#31734,#31735,#31736,
#31737,#31738,#31739,#31740,#31741,#31742,#31743,#31744,#31745,#31746,#31747,
#31748,#31749,#31750,#31751,#31752,#31753,#31754,#31755,#31756,#31757,#31758,
#31759,#31760,#31761,#31762,#31763,#31764,#31765,#31766,#31767,#31768,#31769,
#31770,#31771,#31772),(#31773,#31774,#31775,#31776,#31777,#31778,#31779,
#31780,#31781,#31782,#31783,#31784,#31785,#31786,#31787,#31788,#31789,#31790,
#31791,#31792,#31793,#31794,#31795,#31796,#31797,#31798,#31799,#31800,#31801,
#31802,#31803,#31804,#31805,#31806,#31807,#31808,#31809,#31810,#31811,#31812,
#31813,#31814,#31815,#31816,#31817,#31818,#31819,#31820,#31821,#31822,#31823,
#31824,#31825,#31826,#31827,#31828,#31829,#31830,#31831,#31832,#31833,#31834,
#31835,#31836,#31837,#31838,#31839,#31840,#31841,#31842,#31843,#31844,#31845,
#31846,#31847,#31848,#31849,#31850,#31851,#31852,#31853,#31854,#31855),
(#31856,#31857,#31858,#31859,#31860,#31861,#31862,#31863,#31864,#31865,
#31866,#31867,#31868,#31869,#31870,#31871,#31872,#31873,#31874,#31875,#31876,
#31877,#31878,#31879,#31880,#31881,#31882,#31883,#31884,#31885,#31886,#31887,
#31888,#31889,#31890,#31891,#31892,#31893,#31894,#31895,#31896,#31897,#31898,
#31899,#31900,#31901,#31902,#31903,#31904,#31905,#31906,#31907,#31908,#31909,
#31910,#31911,#31912,#31913,#31914,#31915,#31916,#31917,#31918,#31919,#31920,
#31921,#31922,#31923,#31924,#31925,#31926,#31927,#31928,#31929,#31930,#31931,
#31932,#31933,#31934,#31935,#31936,#31937,#31938),(#31939,#31940,#31941,
#31942,#31943,#31944,#31945,#31946,#31947,#31948,#31949,#31950,#31951,#31952,
#31953,#31954,#31955,#31956,#31957,#31958,#31959,#31960,#31961,#31962,#31963,
#31964,#31965,#31966,#31967,#31968,#31969,#31970,#31971,#31972,#31973,#31974,
#31975,#31976,#31977,#31978,#31979,#31980,#31981,#31982,#31983,#31984,#31985,
#31986,#31987,#31988,#31989,#31990,#31991,#31992,#31993,#31994,#31995,#31996,
#31997,#31998,#31999,#32000,#32001,#32002,#32003,#32004,#32005,#32006,#32007,
#32008,#32009,#32010,#32011,#32012,#32013,#32014,#32015,#32016,#32017,#32018,
#32019,#32020,#32021),(#32022,#32023,#32024,#32025,#32026,#32027,#32028,
#32029,#32030,#32031,#32032,#32033,#32034,#32035,#32036,#32037,#32038,#32039,
#32040,#32041,#32042,#32043,#32044,#32045,#32046,#32047,#32048,#32049,#32050,
#32051,#32052,#32053,#32054,#32055,#32056,#32057,#32058,#32059,#32060,#32061,
#32062,#32063,#32064,#32065,#32066,#32067,#32068,#32069,#32070,#32071,#32072,
#32073,#32074,#32075,#32076,#32077,#32078,#32079,#32080,#32081,#32082,#32083,
#32084,#32085,#32086,#32087,#32088,#32089,#32090,#32091,#32092,#32093,#32094,
#32095,#32096,#32097,#32098,#32099,#32100,#32101,#32102,#32103,#32104)),
 .UNSPECIFIED.,.T.,.F.,.F.,(4,1,1,1,1,1,1,4),(4,1,1,1,1,1,1,1,1,1,1,1,1,
1,1,1,1,1,1,1,1,1,1,1,1,1,1,1,1,1,1,1,1,1,1,1,1,1,1,1,1,1,1,1,1,1,1,1,1,
1,1,1,1,1,1,1,1,1,1,1,1,1,1,1,1,1,1,1,1,1,1,1,1,1,1,1,1,1,1,1,4),(-3.14159265358979,
-2.24399475256414,-1.34639685153848,-0.448798950512828,0.448798950512828,
1.34639685153848,2.24399475256414,3.14159265358979),(0.,0.00892857142857143,
0.0178571428571429,0.0267857142857143,0.0357142857142857,0.0535714285714286,
0.0714285714285714,0.0892857142857143,0.107142857142857,0.125,0.133928571428571,
0.142857142857143,0.158730158730159,0.174603174603175,0.19047619047619,
0.202380952380952,0.214285714285714,0.226190476190476,0.238095238095238,
0.25,0.261904761904762,0.273809523809524,0.279761904761905,0.285714285714286,
0.297619047619048,0.30952380952381,0.321428571428571,0.333333333333333,
0.349206349206349,0.365079365079365,0.373015873015873,0.380952380952381,
0.396825396825397,0.412698412698413,0.428571428571429,0.444444444444444,
0.46031746031746,0.476190476190476,0.492063492063492,0.507936507936508,
0.523809523809524,0.535714285714286,0.547619047619048,0.55952380952381,
0.571428571428571,0.583333333333333,0.595238095238095,0.607142857142857,
0.619047619047619,0.630952380952381,0.642857142857143,0.654761904761905,
0.666666666666667,0.682539682539682,0.698412698412698,0.706349206349206,
0.714285714285714,0.722222222222222,0.73015873015873,0.746031746031746,
0.761904761904762,0.773809523809524,0.785714285714286,0.797619047619047,
0.809523809523809,0.821428571428571,0.833333333333333,0.845238095238095,
0.857142857142857,0.861607142857143,0.866071428571429,0.875,0.892857142857143,
0.910714285714286,0.928571428571429,0.946428571428571,0.964285714285714,
0.973214285714286,0.982142857142857,0.991071428571429,1.),.UNSPECIFIED.);
#577=B_SPLINE_CURVE_WITH_KNOTS('',3,(#31189,#31190,#31191,#31192,#31193,
#31194,#31195,#31196,#31197,#31198,#31199,#31200,#31201,#31202,#31203,#31204,
#31205,#31206,#31207,#31208,#31209,#31210,#31211,#31212,#31213,#31214,#31215,
#31216,#31217,#31218,#31219,#31220,#31221,#31222,#31223,#31224),
 .UNSPECIFIED.,.F.,.F.,(4,2,2,2,2,2,2,2,2,2,2,2,2,2,2,2,2,4),(-8.09601808660967,
-6.95211114501378,-5.94311837811659,-4.55541281139976,-3.41582959923829,
-3.01501785802626,-2.8942748329529,-2.84936482218812,-2.82500498483727,
-2.8058948573567,-2.78504274409744,-2.75364696269285,-2.68586477663438,
-2.5294569358349,-2.14040235758073,-1.34382220888079,-0.648089834050052,
0.),.UNSPECIFIED.);
#578=B_SPLINE_CURVE_WITH_KNOTS('',3,(#31233,#31234,#31235,#31236,#31237,
#31238,#31239,#31240,#31241,#31242,#31243,#31244,#31245,#31246,#31247,#31248),
 .UNSPECIFIED.,.F.,.F.,(4,2,2,2,2,2,2,4),(-8.25962359305892,-7.06880639418565,
-6.02569177482105,-4.59002353937466,-3.42632229394732,-3.02472929447217,
-2.902401118056,-2.8848490611025),.UNSPECIFIED.);
#579=B_SPLINE_CURVE_WITH_KNOTS('',3,(#31251,#31252,#31253,#31254,#31255,
#31256,#31257,#31258,#31259,#31260,#31261,#31262,#31263,#31264,#31265,#31266,
#31267,#31268,#31269,#31270,#31271,#31272),.UNSPECIFIED.,.F.,.F.,(4,2,2,
2,2,2,2,2,2,2,4),(-2.8848490611025,-2.85598304066293,-2.83035400420251,
-2.80984607017121,-2.78716062094501,-2.75249343197851,-2.66253946470509,
-2.14039903787906,-1.34382126836984,-0.648090922770533,0.),
 .UNSPECIFIED.);
#580=B_SPLINE_CURVE_WITH_KNOTS('',3,(#32105,#32106,#32107,#32108,#32109,
#32110,#32111,#32112,#32113,#32114,#32115,#32116,#32117,#32118,#32119,#32120,
#32121,#32122,#32123,#32124,#32125,#32126,#32127,#32128,#32129,#32130,#32131,
#32132,#32133,#32134,#32135,#32136,#32137,#32138,#32139,#32140,#32141,#32142,
#32143,#32144,#32145,#32146,#32147,#32148,#32149,#32150,#32151,#32152,#32153,
#32154,#32155,#32156,#32157,#32158,#32159,#32160,#32161,#32162,#32163,#32164,
#32165,#32166,#32167,#32168,#32169,#32170,#32171,#32172,#32173,#32174,#32175,
#32176,#32177,#32178,#32179,#32180,#32181,#32182,#32183,#32184),
 .UNSPECIFIED.,.F.,.F.,(4,1,1,1,1,1,1,1,1,1,1,1,1,1,1,1,1,1,1,1,1,1,1,1,
1,1,1,1,1,1,1,1,1,1,1,1,1,1,1,1,1,1,1,1,1,1,1,1,1,1,1,1,1,1,1,1,1,1,1,1,
1,1,1,1,1,1,1,1,1,1,1,1,1,1,1,1,1,4),(0.0345080125489109,0.0357142857142857,
0.0535714285714286,0.0714285714285714,0.0892857142857143,0.107142857142857,
0.125,0.133928571428571,0.142857142857143,0.158730158730159,0.174603174603175,
0.19047619047619,0.202380952380952,0.214285714285714,0.226190476190476,
0.238095238095238,0.25,0.261904761904762,0.273809523809524,0.279761904761905,
0.285714285714286,0.297619047619048,0.30952380952381,0.321428571428571,
0.333333333333333,0.349206349206349,0.365079365079365,0.373015873015873,
0.380952380952381,0.396825396825397,0.412698412698413,0.428571428571429,
0.444444444444444,0.46031746031746,0.476190476190476,0.492063492063492,
0.507936507936508,0.523809523809524,0.535714285714286,0.547619047619048,
0.55952380952381,0.571428571428571,0.583333333333333,0.595238095238095,
0.607142857142857,0.619047619047619,0.630952380952381,0.642857142857143,
0.654761904761905,0.666666666666667,0.682539682539682,0.698412698412698,
0.706349206349206,0.714285714285714,0.722222222222222,0.73015873015873,
0.746031746031746,0.761904761904762,0.773809523809524,0.785714285714286,
0.797619047619047,0.809523809523809,0.821428571428571,0.833333333333333,
0.845238095238095,0.857142857142857,0.861607142857143,0.866071428571429,
0.875,0.892857142857143,0.910714285714286,0.928571428571429,0.946428571428571,
0.964285714285714,0.973214285714286,0.982142857142857,0.991071428571429,
1.),.UNSPECIFIED.);
#1511=SHAPE_REPRESENTATION_RELATIONSHIP('SRR','None',#59300,#1531);
#1531=ADVANCED_BREP_SHAPE_REPRESENTATION('',(#1578),#59187);
#1551=STYLED_ITEM('',(#59586),#1578);
#1578=MANIFOLD_SOLID_BREP('Spring',#22807);
#1821=PLANE('',#23167);
#1822=PLANE('',#23168);
#1823=PLANE('',#23171);
#1824=PLANE('',#23172);
#2727=FACE_OUTER_BOUND('',#4057,.T.);
#2728=FACE_OUTER_BOUND('',#4058,.T.);
#2729=FACE_OUTER_BOUND('',#4059,.T.);
#2730=FACE_OUTER_BOUND('',#4060,.T.);
#2731=FACE_OUTER_BOUND('',#4061,.T.);
#4057=EDGE_LOOP('',(#14918,#14919));
#4058=EDGE_LOOP('',(#14920,#14921,#14922));
#4059=EDGE_LOOP('',(#14923,#14924,#14925));
#4060=EDGE_LOOP('',(#14926,#14927));
#4061=EDGE_LOOP('',(#14928,#14929,#14930,#14931,#14932,#14933,#14934,#14935));
#5546=LINE('',#31225,#6979);
#5547=LINE('',#31250,#6980);
#6979=VECTOR('',#25418,1.);
#6980=VECTOR('',#25427,1.);
#8418=CIRCLE('',#23169,0.15);
#8419=CIRCLE('',#23170,0.15);
#8420=CIRCLE('',#23173,0.15);
#9269=VERTEX_POINT('',#31187);
#9270=VERTEX_POINT('',#31188);
#9271=VERTEX_POINT('',#31227);
#9272=VERTEX_POINT('',#31231);
#9273=VERTEX_POINT('',#31232);
#9274=VERTEX_POINT('',#31249);
#11463=EDGE_CURVE('',#9269,#9270,#577,.T.);
#11464=EDGE_CURVE('',#9270,#9269,#5546,.T.);
#11465=EDGE_CURVE('',#9269,#9271,#8418,.T.);
#11466=EDGE_CURVE('',#9271,#9270,#8419,.T.);
#11467=EDGE_CURVE('',#9272,#9273,#578,.T.);
#11468=EDGE_CURVE('',#9274,#9272,#5547,.T.);
#11469=EDGE_CURVE('',#9273,#9274,#579,.T.);
#11470=EDGE_CURVE('',#9274,#9272,#8420,.T.);
#11471=EDGE_CURVE('',#9273,#9271,#580,.T.);
#14918=ORIENTED_EDGE('',*,*,#11463,.F.);
#14919=ORIENTED_EDGE('',*,*,#11464,.F.);
#14920=ORIENTED_EDGE('',*,*,#11464,.T.);
#14921=ORIENTED_EDGE('',*,*,#11465,.T.);
#14922=ORIENTED_EDGE('',*,*,#11466,.T.);
#14923=ORIENTED_EDGE('',*,*,#11467,.F.);
#14924=ORIENTED_EDGE('',*,*,#11468,.F.);
#14925=ORIENTED_EDGE('',*,*,#11469,.F.);
#14926=ORIENTED_EDGE('',*,*,#11468,.T.);
#14927=ORIENTED_EDGE('',*,*,#11470,.F.);
#14928=ORIENTED_EDGE('',*,*,#11463,.T.);
#14929=ORIENTED_EDGE('',*,*,#11466,.F.);
#14930=ORIENTED_EDGE('',*,*,#11471,.F.);
#14931=ORIENTED_EDGE('',*,*,#11469,.T.);
#14932=ORIENTED_EDGE('',*,*,#11470,.T.);
#14933=ORIENTED_EDGE('',*,*,#11467,.T.);
#14934=ORIENTED_EDGE('',*,*,#11471,.T.);
#14935=ORIENTED_EDGE('',*,*,#11465,.F.);
#21557=ADVANCED_FACE('',(#2727),#1821,.T.);
#21558=ADVANCED_FACE('',(#2728),#1822,.T.);
#21559=ADVANCED_FACE('',(#2729),#1823,.F.);
#21560=ADVANCED_FACE('',(#2730),#1824,.F.);
#21561=ADVANCED_FACE('',(#2731),#317,.T.);
#22807=CLOSED_SHELL('',(#21557,#21558,#21559,#21560,#21561));
#23166=AXIS2_PLACEMENT_3D('',#31185,#25414,#25415);
#23167=AXIS2_PLACEMENT_3D('',#31186,#25416,#25417);
#23168=AXIS2_PLACEMENT_3D('',#31226,#25419,#25420);
#23169=AXIS2_PLACEMENT_3D('',#31228,#25421,#25422);
#23170=AXIS2_PLACEMENT_3D('',#31229,#25423,#25424);
#23171=AXIS2_PLACEMENT_3D('',#31230,#25425,#25426);
#23172=AXIS2_PLACEMENT_3D('',#31273,#25428,#25429);
#23173=AXIS2_PLACEMENT_3D('',#31274,#25430,#25431);
#25414=DIRECTION('axis',(0.,0.,1.));
#25415=DIRECTION('refdir',(1.,0.,0.));
#25416=DIRECTION('center_axis',(0.,0.,1.));
#25417=DIRECTION('ref_axis',(1.,0.,0.));
#25418=DIRECTION('',(-0.999993517565735,0.00360067028606715,0.));
#25419=DIRECTION('center_axis',(-0.00359876467778075,-0.999464283900328,
0.0325298954870402));
#25420=DIRECTION('ref_axis',(0.99824685088558,-0.00166873393288522,0.0591645165963828));
#25421=DIRECTION('center_axis',(-0.00359876467778075,-0.999464283900328,
0.0325298954870402));
#25422=DIRECTION('ref_axis',(0.99824685088558,-0.00166873393288521,0.0591645165963828));
#25423=DIRECTION('center_axis',(-0.00359876467778075,-0.999464283900328,
0.0325298954870402));
#25424=DIRECTION('ref_axis',(0.99824685088558,-0.00166873393288521,0.0591645165963828));
#25425=DIRECTION('center_axis',(0.,0.,1.));
#25426=DIRECTION('ref_axis',(1.,0.,0.));
#25427=DIRECTION('',(0.999993517565781,0.00360067027305193,0.));
#25428=DIRECTION('center_axis',(-0.00359876466477833,0.999464283902014,
0.0325298954366743));
#25429=DIRECTION('ref_axis',(0.000117129427484697,-0.032529684563767,0.999470762905489));
#25430=DIRECTION('center_axis',(-0.00359876466477833,0.999464283902014,
0.0325298954366743));
#25431=DIRECTION('ref_axis',(0.000117129427484697,-0.032529684563767,0.999470762905488));
#31185=CARTESIAN_POINT('',(0.,0.,0.));
#31186=CARTESIAN_POINT('Origin',(0.,0.,-2.));
#31187=CARTESIAN_POINT('',(-1.61995291789844,0.00336117355255646,-2.));
#31188=CARTESIAN_POINT('',(-1.38002598764053,0.00249727018375272,-2.));
#31189=CARTESIAN_POINT('Ctrl Pts',(-1.61995291789844,0.00336117355255575,
-2.));
#31190=CARTESIAN_POINT('Ctrl Pts',(-1.61549424307396,0.162481506613328,
-2.));
#31191=CARTESIAN_POINT('Ctrl Pts',(-1.58875419089395,0.318012758496866,
-1.9999999999982));
#31192=CARTESIAN_POINT('Ctrl Pts',(-1.49275027839831,0.601309372298675,
-1.9999999999982));
#31193=CARTESIAN_POINT('Ctrl Pts',(-1.42966216744865,0.727509819034175,
-2.));
#31194=CARTESIAN_POINT('Ctrl Pts',(-1.24263066606898,1.00185310345563,-2.));
#31195=CARTESIAN_POINT('Ctrl Pts',(-1.10452674883175,1.14075648283468,-2.));
#31196=CARTESIAN_POINT('Ctrl Pts',(-0.812893641026086,1.33182547339981,
-2.));
#31197=CARTESIAN_POINT('Ctrl Pts',(-0.695845885242561,1.37569431979837,
-2.));
#31198=CARTESIAN_POINT('Ctrl Pts',(-0.600973807488825,1.39942220003299,
-2.));
#31199=CARTESIAN_POINT('Ctrl Pts',(-0.58060683846439,1.40270563705104,-2.));
#31200=CARTESIAN_POINT('Ctrl Pts',(-0.562399803406437,1.40311353681833,
-2.));
#31201=CARTESIAN_POINT('Ctrl Pts',(-0.557327933391125,1.40297057403271,
-2.));
#31202=CARTESIAN_POINT('Ctrl Pts',(-0.551673715306211,1.40166051391577,
-2.));
#31203=CARTESIAN_POINT('Ctrl Pts',(-0.550045660231946,1.40114098270715,
-2.));
#31204=CARTESIAN_POINT('Ctrl Pts',(-0.547931698369792,1.39993820927597,
-2.));
#31205=CARTESIAN_POINT('Ctrl Pts',(-0.547229470490149,1.39941927367039,
-2.));
#31206=CARTESIAN_POINT('Ctrl Pts',(-0.5462173517456,1.39827575338564,-2.));
#31207=CARTESIAN_POINT('Ctrl Pts',(-0.545868566103154,1.39771288260701,
-2.));
#31208=CARTESIAN_POINT('Ctrl Pts',(-0.545387398917564,1.3963939753859,-2.));
#31209=CARTESIAN_POINT('Ctrl Pts',(-0.545296117033786,1.39567565836781,
-2.));
#31210=CARTESIAN_POINT('Ctrl Pts',(-0.545376025403559,1.39384190830807,
-2.));
#31211=CARTESIAN_POINT('Ctrl Pts',(-0.545702512867774,1.39273799453804,
-2.00000000000012));
#31212=CARTESIAN_POINT('Ctrl Pts',(-0.547062395356521,1.38953579204815,
-2.00000000000012));
#31213=CARTESIAN_POINT('Ctrl Pts',(-0.548723311267636,1.38718205745838,
-2.));
#31214=CARTESIAN_POINT('Ctrl Pts',(-0.555563352310482,1.37927028912354,
-2.));
#31215=CARTESIAN_POINT('Ctrl Pts',(-0.563225688718851,1.37271906642457,
-2.));
#31216=CARTESIAN_POINT('Ctrl Pts',(-0.597143575123905,1.34688019040191,
-2.));
#31217=CARTESIAN_POINT('Ctrl Pts',(-0.634475174910193,1.32279953682347,
-1.99999999999601));
#31218=CARTESIAN_POINT('Ctrl Pts',(-0.773754982438386,1.22649039949967,
-1.99999999999601));
#31219=CARTESIAN_POINT('Ctrl Pts',(-0.90401491384939,1.12926273899443,-2.00000000000043));
#31220=CARTESIAN_POINT('Ctrl Pts',(-1.13965675392752,0.850355239559298,
-2.00000000000043));
#31221=CARTESIAN_POINT('Ctrl Pts',(-1.22749032481239,0.702921990413554,
-1.99999999999073));
#31222=CARTESIAN_POINT('Ctrl Pts',(-1.34378737767206,0.396439291894907,
-1.99999999999073));
#31223=CARTESIAN_POINT('Ctrl Pts',(-1.38452169713765,0.218480430629212,
-2.));
#31224=CARTESIAN_POINT('Ctrl Pts',(-1.38002598764053,0.00249727018375276,
-2.));
#31225=CARTESIAN_POINT('',(-0.749999176389368,0.000228736659435569,-2.));
#31226=CARTESIAN_POINT('Origin',(-1.5,7.2997163869104E-15,-2.09));
#31227=CARTESIAN_POINT('',(-1.64973702763284,0.000250310089940087,-2.09887467748946));
#31228=CARTESIAN_POINT('Origin',(-1.5,7.2997163869104E-15,-2.09));
#31229=CARTESIAN_POINT('Origin',(-1.5,7.2997163869104E-15,-2.09));
#31230=CARTESIAN_POINT('Origin',(0.,0.,-4.45));
#31231=CARTESIAN_POINT('',(1.61995291789861,0.00336117354644825,-4.45));
#31232=CARTESIAN_POINT('',(0.551181637679476,1.40145119755991,-4.44999999999997));
#31233=CARTESIAN_POINT('Ctrl Pts',(1.61995291789861,0.00336117354644749,
-4.45));
#31234=CARTESIAN_POINT('Ctrl Pts',(1.61528760482228,0.169855973259341,-4.45));
#31235=CARTESIAN_POINT('Ctrl Pts',(1.58623246551132,0.3322543098989,-4.45000000000239));
#31236=CARTESIAN_POINT('Ctrl Pts',(1.48200312795181,0.626180370842875,-4.45000000000239));
#31237=CARTESIAN_POINT('Ctrl Pts',(1.41386708572138,0.756188302107039,-4.45));
#31238=CARTESIAN_POINT('Ctrl Pts',(1.21256653981921,1.03640064697837,-4.45));
#31239=CARTESIAN_POINT('Ctrl Pts',(1.07053138485629,1.16765933441729,-4.45));
#31240=CARTESIAN_POINT('Ctrl Pts',(0.793916964682515,1.33970036291334,-4.45));
#31241=CARTESIAN_POINT('Ctrl Pts',(0.685050094788204,1.37914609751066,-4.45));
#31242=CARTESIAN_POINT('Ctrl Pts',(0.597251719842088,1.40004655942463,-4.45));
#31243=CARTESIAN_POINT('Ctrl Pts',(0.578519790624767,1.40289555289961,-4.45));
#31244=CARTESIAN_POINT('Ctrl Pts',(0.561493394806395,1.40308177478702,-4.45));
#31245=CARTESIAN_POINT('Ctrl Pts',(0.556741538198221,1.40288720515261,-4.45));
#31246=CARTESIAN_POINT('Ctrl Pts',(0.552311123311035,1.40179794647584,-4.45));
#31247=CARTESIAN_POINT('Ctrl Pts',(0.551743404220043,1.40163840793096,-4.45));
#31248=CARTESIAN_POINT('Ctrl Pts',(0.551181637679889,1.40145119755868,-4.45));
#31249=CARTESIAN_POINT('',(1.38002598764047,0.00249727018076643,-4.45));
#31250=CARTESIAN_POINT('',(0.749999176389352,0.000228736664649523,-4.45));
#31251=CARTESIAN_POINT('Ctrl Pts',(0.551181637679889,1.40145119755868,-4.45));
#31252=CARTESIAN_POINT('Ctrl Pts',(0.550257759386119,1.40114331236624,-4.45));
#31253=CARTESIAN_POINT('Ctrl Pts',(0.549350029564563,1.40076043740895,-4.45));
#31254=CARTESIAN_POINT('Ctrl Pts',(0.547815734993885,1.39985605892706,-4.45));
#31255=CARTESIAN_POINT('Ctrl Pts',(0.547138554067502,1.39933713661373,-4.45));
#31256=CARTESIAN_POINT('Ctrl Pts',(0.546158473208201,1.39819032015798,-4.45));
#31257=CARTESIAN_POINT('Ctrl Pts',(0.545822053337169,1.39762167328648,-4.45));
#31258=CARTESIAN_POINT('Ctrl Pts',(0.54536469712454,1.39628540347643,-4.45));
#31259=CARTESIAN_POINT('Ctrl Pts',(0.54528822880981,1.39555505046602,-4.45));
#31260=CARTESIAN_POINT('Ctrl Pts',(0.545406200377944,1.3936835057743,-4.45));
#31261=CARTESIAN_POINT('Ctrl Pts',(0.545764203801092,1.39255134723921,-4.4499999999995));
#31262=CARTESIAN_POINT('Ctrl Pts',(0.547413677033348,1.38883263821314,-4.4499999999995));
#31263=CARTESIAN_POINT('Ctrl Pts',(0.549725166268199,1.38580722469121,-4.45));
#31264=CARTESIAN_POINT('Ctrl Pts',(0.570820183212706,1.36368371960921,-4.45));
#31265=CARTESIAN_POINT('Ctrl Pts',(0.618842346650772,1.33360936522388,-4.45));
#31266=CARTESIAN_POINT('Ctrl Pts',(0.77375649475805,1.22648928125047,-4.45));
#31267=CARTESIAN_POINT('Ctrl Pts',(0.904015969469336,1.12926165467428,-4.45000000000126));
#31268=CARTESIAN_POINT('Ctrl Pts',(1.13965686376268,0.850354965350669,-4.45000000000126));
#31269=CARTESIAN_POINT('Ctrl Pts',(1.22749013747112,0.702922208817644,-4.45));
#31270=CARTESIAN_POINT('Ctrl Pts',(1.34378724077005,0.39643990907693,-4.45));
#31271=CARTESIAN_POINT('Ctrl Pts',(1.38452170468453,0.218480793454572,-4.45));
#31272=CARTESIAN_POINT('Ctrl Pts',(1.38002598764047,0.00249727018076639,
-4.45));
#31273=CARTESIAN_POINT('Origin',(1.5,2.69411970987176E-17,-4.36));
#31274=CARTESIAN_POINT('Origin',(1.5,2.69411970987176E-17,-4.36));
#31275=CARTESIAN_POINT('Ctrl Pts',(1.49998243058588,0.00487945268456504,
-4.50992061443582));
#31276=CARTESIAN_POINT('Ctrl Pts',(1.49941141170999,0.163465252269264,-4.50475906983506));
#31277=CARTESIAN_POINT('Ctrl Pts',(1.45186405026655,0.468260659554012,-4.49443439156157));
#31278=CARTESIAN_POINT('Ctrl Pts',(1.24285849641208,0.886559230778761,-4.47894878298098));
#31279=CARTESIAN_POINT('Ctrl Pts',(0.914832037666938,1.22538627239788,-4.46342570918691));
#31280=CARTESIAN_POINT('Ctrl Pts',(0.362526476214984,1.52015190223001,-4.44275032349895));
#31281=CARTESIAN_POINT('Ctrl Pts',(-0.450285458827622,1.54477765231458,
-4.41673352060185));
#31282=CARTESIAN_POINT('Ctrl Pts',(-1.26358566414186,1.00029259499041,-4.38579230410963));
#31283=CARTESIAN_POINT('Ctrl Pts',(-1.61297063863451,0.0851696210599042,
-4.35408217822798));
#31284=CARTESIAN_POINT('Ctrl Pts',(-1.36691769149066,-0.86636719535778,
-4.32382427572184));
#31285=CARTESIAN_POINT('Ctrl Pts',(-0.740664712301201,-1.39406711347056,
-4.29568368658589));
#31286=CARTESIAN_POINT('Ctrl Pts',(-0.123568561445898,-1.54231629531191,
-4.27827259231965));
#31287=CARTESIAN_POINT('Ctrl Pts',(0.477570602247783,-1.50045464230821,
-4.25010620760684));
#31288=CARTESIAN_POINT('Ctrl Pts',(1.12799462557692,-1.14561364539286,-4.21523812123688));
#31289=CARTESIAN_POINT('Ctrl Pts',(1.56388513724472,-0.389673012803625,
-4.17546007003578));
#31290=CARTESIAN_POINT('Ctrl Pts',(1.5433188232119,0.410763669941787,-4.13857735821636));
#31291=CARTESIAN_POINT('Ctrl Pts',(1.19490853879333,1.03893941579882,-4.10508910882579));
#31292=CARTESIAN_POINT('Ctrl Pts',(0.681279880783051,1.43269210784687,-4.07487536403218));
#31293=CARTESIAN_POINT('Ctrl Pts',(0.051646821861207,1.58859643745763,-4.04459309324451));
#31294=CARTESIAN_POINT('Ctrl Pts',(-0.588862535961304,1.47930900476985,
-4.01426969238989));
#31295=CARTESIAN_POINT('Ctrl Pts',(-1.13322870809872,1.1225062752352,-3.98388228335323));
#31296=CARTESIAN_POINT('Ctrl Pts',(-1.4902067993283,0.576759659588736,-3.95344539501966));
#31297=CARTESIAN_POINT('Ctrl Pts',(-1.58102020223693,0.0400740757948976,
-3.92803411508518));
#31298=CARTESIAN_POINT('Ctrl Pts',(-1.52052962309553,-0.384828263720139,
-3.90767925424071));
#31299=CARTESIAN_POINT('Ctrl Pts',(-1.3748830928401,-0.788957250234775,
-3.88730621071591));
#31300=CARTESIAN_POINT('Ctrl Pts',(-1.0423371162911,-1.22218867468557,-3.86180720794638));
#31301=CARTESIAN_POINT('Ctrl Pts',(-0.467378790598492,-1.53972799805516,
-3.83115568482052));
#31302=CARTESIAN_POINT('Ctrl Pts',(0.187274531141039,-1.60068158914455,
-3.80045226057647));
#31303=CARTESIAN_POINT('Ctrl Pts',(0.883096272461548,-1.37238382842803,
-3.76628010013367));
#31304=CARTESIAN_POINT('Ctrl Pts',(1.45542862121288,-0.785128737057825,
-3.72861800828645));
#31305=CARTESIAN_POINT('Ctrl Pts',(1.62183852895481,-0.0567398924127903,
-3.69430530328978));
#31306=CARTESIAN_POINT('Ctrl Pts',(1.51242393883133,0.515046269014153,-3.66681113832745));
#31307=CARTESIAN_POINT('Ctrl Pts',(1.25371395215128,1.0371419048164,-3.63928782397711));
#31308=CARTESIAN_POINT('Ctrl Pts',(0.679041108905056,1.51956040430477,-3.60482953394523));
#31309=CARTESIAN_POINT('Ctrl Pts',(-0.213247562120534,1.65433450298338,
-3.56339447382386));
#31310=CARTESIAN_POINT('Ctrl Pts',(-1.04680323812526,1.30346814108,-3.52187569315801));
#31311=CARTESIAN_POINT('Ctrl Pts',(-1.57557751626781,0.567442201034068,
-3.48027478133792));
#31312=CARTESIAN_POINT('Ctrl Pts',(-1.64318830952972,-0.337637019006298,
-3.43859332018342));
#31313=CARTESIAN_POINT('Ctrl Pts',(-1.22844519515377,-1.14714492715669,
-3.39683307764518));
#31314=CARTESIAN_POINT('Ctrl Pts',(-0.451245980735406,-1.62215680765017,
-3.35499576544402));
#31315=CARTESIAN_POINT('Ctrl Pts',(0.461841974941765,-1.62319460304399,
-3.31308315566976));
#31316=CARTESIAN_POINT('Ctrl Pts',(1.17649440309474,-1.18543555842648,-3.27459582000513));
#31317=CARTESIAN_POINT('Ctrl Pts',(1.5636738872075,-0.54221871976191,-3.23955517618414));
#31318=CARTESIAN_POINT('Ctrl Pts',(1.65231581225766,0.128238780519003,-3.20797910267182));
#31319=CARTESIAN_POINT('Ctrl Pts',(1.46493973472583,0.779138006438161,-3.17636441807156));
#31320=CARTESIAN_POINT('Ctrl Pts',(1.03253139188493,1.30136595938992,-3.14471191495533));
#31321=CARTESIAN_POINT('Ctrl Pts',(0.426609970086491,1.60751024918497,-3.11302251069183));
#31322=CARTESIAN_POINT('Ctrl Pts',(-0.251933879032834,1.64584505089144,
-3.08129700553233));
#31323=CARTESIAN_POINT('Ctrl Pts',(-0.889905805470703,1.40942555957253,
-3.04953632759992));
#31324=CARTESIAN_POINT('Ctrl Pts',(-1.38068331350981,0.937053401938582,
-3.01774135131172));
#31325=CARTESIAN_POINT('Ctrl Pts',(-1.64184179716058,0.307317409087506,
-2.98591300518706));
#31326=CARTESIAN_POINT('Ctrl Pts',(-1.62957916709941,-0.37530803509689,
-2.95405221275351));
#31327=CARTESIAN_POINT('Ctrl Pts',(-1.34474730528677,-0.996034495385219,
-2.92215989404433));
#31328=CARTESIAN_POINT('Ctrl Pts',(-0.778879409529726,-1.50350912987896,
-2.88668999089474));
#31329=CARTESIAN_POINT('Ctrl Pts',(0.0452156959044932,-1.71370006437942,
-2.84763094470004));
#31330=CARTESIAN_POINT('Ctrl Pts',(0.785100365893931,-1.486208751186,-2.81208062847635));
#31331=CARTESIAN_POINT('Ctrl Pts',(1.24161679713701,-1.09259013745182,-2.7836165314676));
#31332=CARTESIAN_POINT('Ctrl Pts',(1.49217131201598,-0.716178712962469,
-2.76225639002869));
#31333=CARTESIAN_POINT('Ctrl Pts',(1.63085414425123,-0.285537734548898,
-2.7408855262812));
#31334=CARTESIAN_POINT('Ctrl Pts',(1.65475200752033,0.317728375257333,-2.7123738937245));
#31335=CARTESIAN_POINT('Ctrl Pts',(1.37145521865962,1.04076278423927,-2.67671479060714));
#31336=CARTESIAN_POINT('Ctrl Pts',(0.69041646931577,1.55777895441666,-2.63743464573646));
#31337=CARTESIAN_POINT('Ctrl Pts',(-0.0643948515707663,1.68574777587918,
-2.6017316079884));
#31338=CARTESIAN_POINT('Ctrl Pts',(-0.733422672005601,1.52073388540773,
-2.56950115646222));
#31339=CARTESIAN_POINT('Ctrl Pts',(-1.28085476582717,1.10113604465525,-2.53741554342871));
#31340=CARTESIAN_POINT('Ctrl Pts',(-1.61517951924605,0.4975562304161,-2.50499073603886));
#31341=CARTESIAN_POINT('Ctrl Pts',(-1.68029840248005,-0.189791143389858,
-2.47314557601871));
#31342=CARTESIAN_POINT('Ctrl Pts',(-1.46497737904047,-0.846156793246451,
-2.44020210847229));
#31343=CARTESIAN_POINT('Ctrl Pts',(-1.00508021286665,-1.36188270355857,
-2.40899190246463));
#31344=CARTESIAN_POINT('Ctrl Pts',(-0.507582321376923,-1.59058364540096,
-2.38240038156976));
#31345=CARTESIAN_POINT('Ctrl Pts',(-0.115985349294589,-1.64889286597431,
-2.36303576958252));
#31346=CARTESIAN_POINT('Ctrl Pts',(0.223158570335046,-1.64681924620263,
-2.349562123073));
#31347=CARTESIAN_POINT('Ctrl Pts',(0.806901355148856,-1.50671742388011,
-2.33231544041505));
#31348=CARTESIAN_POINT('Ctrl Pts',(1.48644477626825,-0.934917871941825,
-2.30237235343056));
#31349=CARTESIAN_POINT('Ctrl Pts',(1.75362331696032,0.0983401101520701,
-2.26920259215576));
#31350=CARTESIAN_POINT('Ctrl Pts',(1.37388207698597,1.09486845045221,-2.23481640537456));
#31351=CARTESIAN_POINT('Ctrl Pts',(0.486437491100621,1.68918937268853,-2.20098350021554));
#31352=CARTESIAN_POINT('Ctrl Pts',(-0.402275175720241,1.66276347810902,
-2.172565595614));
#31353=CARTESIAN_POINT('Ctrl Pts',(-1.0075498708897,1.33971834323449,-2.14990060001603));
#31354=CARTESIAN_POINT('Ctrl Pts',(-1.36740441992316,0.968073875003734,
-2.13287342310861));
#31355=CARTESIAN_POINT('Ctrl Pts',(-1.59664060478066,0.509453342147398,
-2.11589441486025));
#31356=CARTESIAN_POINT('Ctrl Pts',(-1.64911395659225,0.173292258411803,
-2.10450673116507));
#31357=CARTESIAN_POINT('Ctrl Pts',(-1.64973702763284,0.000250310089940127,
-2.09887467748946));
#31358=CARTESIAN_POINT('Ctrl Pts',(1.45510282646556,0.00471785498059619,
-4.50992061443582));
#31359=CARTESIAN_POINT('Ctrl Pts',(1.45454752466905,0.158938640195152,-4.50490113940505));
#31360=CARTESIAN_POINT('Ctrl Pts',(1.40849772159958,0.454254551280147,-4.4948981491038));
#31361=CARTESIAN_POINT('Ctrl Pts',(1.20562360660865,0.860308403854419,-4.47986552905065));
#31362=CARTESIAN_POINT('Ctrl Pts',(0.887402599021796,1.18901004224185,-4.4648071396859));
#31363=CARTESIAN_POINT('Ctrl Pts',(0.351571093928312,1.47496328750251,-4.44474869215259));
#31364=CARTESIAN_POINT('Ctrl Pts',(-0.437170053702789,1.49892968332643,
-4.41950289723679));
#31365=CARTESIAN_POINT('Ctrl Pts',(-1.22639094877331,0.970527058656368,
-4.38947856346812));
#31366=CARTESIAN_POINT('Ctrl Pts',(-1.56553430420601,0.0823976185849323,
-4.35870345993953));
#31367=CARTESIAN_POINT('Ctrl Pts',(-1.32668502908212,-0.841248004046866,
-4.3293339124924));
#31368=CARTESIAN_POINT('Ctrl Pts',(-0.718804245962794,-1.3535248584667,
-4.30201769448259));
#31369=CARTESIAN_POINT('Ctrl Pts',(-0.119616083437381,-1.49748731273866,
-4.28511330421243));
#31370=CARTESIAN_POINT('Ctrl Pts',(0.464392315734694,-1.45682492507003,
-4.25775092153805));
#31371=CARTESIAN_POINT('Ctrl Pts',(1.09590581605906,-1.11228111397,-4.22389805157936));
#31372=CARTESIAN_POINT('Ctrl Pts',(1.51943003519238,-0.377938979423637,
-4.18525403699039));
#31373=CARTESIAN_POINT('Ctrl Pts',(1.49945180577348,0.399795741367386,-4.14941989597277));
#31374=CARTESIAN_POINT('Ctrl Pts',(1.16087569397544,1.01030847094984,-4.11687476750201));
#31375=CARTESIAN_POINT('Ctrl Pts',(0.661597764502885,1.3930744361422,-4.08750627336111));
#31376=CARTESIAN_POINT('Ctrl Pts',(0.0494009166153912,1.54468470898889,
-4.05806288385645));
#31377=CARTESIAN_POINT('Ctrl Pts',(-0.573489867817984,1.43841917455019,
-4.02857543250609));
#31378=CARTESIAN_POINT('Ctrl Pts',(-1.1030291321629,1.09136473006051,-3.99901773693845));
#31379=CARTESIAN_POINT('Ctrl Pts',(-1.45037403297912,0.560371410645132,
-3.96940462755079));
#31380=CARTESIAN_POINT('Ctrl Pts',(-1.53876993207835,0.0380711920125209,
-3.94467586616708));
#31381=CARTESIAN_POINT('Ctrl Pts',(-1.47988735353637,-0.375559805356409,
-3.92486153483449));
#31382=CARTESIAN_POINT('Ctrl Pts',(-1.33809000327692,-0.769022130747614,
-3.90502683865905));
#31383=CARTESIAN_POINT('Ctrl Pts',(-1.01429688563516,-1.19088230653178,
-3.88019939660311));
#31384=CARTESIAN_POINT('Ctrl Pts',(-0.454279919642091,-1.50020353066735,
-3.85034542265613));
#31385=CARTESIAN_POINT('Ctrl Pts',(0.183559018927454,-1.55960563373112,
-3.82043199601657));
#31386=CARTESIAN_POINT('Ctrl Pts',(0.861714986247691,-1.33714723859362,
-3.78713056579467));
#31387=CARTESIAN_POINT('Ctrl Pts',(1.4197478806152,-0.764603217162326,-3.75041228389878));
#31388=CARTESIAN_POINT('Ctrl Pts',(1.58212224236173,-0.0541615033134914,
-3.71694606817844));
#31389=CARTESIAN_POINT('Ctrl Pts',(1.47536678436316,0.503744741559664,-3.69012109357611));
#31390=CARTESIAN_POINT('Ctrl Pts',(1.2228858711314,1.01330066058605,-3.66325987802185));
#31391=CARTESIAN_POINT('Ctrl Pts',(0.661929474527082,1.48426168834351,-3.62962626014974));
#31392=CARTESIAN_POINT('Ctrl Pts',(-0.209612810380294,1.61597543556883,
-3.58915502450247));
#31393=CARTESIAN_POINT('Ctrl Pts',(-1.02416860071843,1.27316933612582,-3.54858706369704));
#31394=CARTESIAN_POINT('Ctrl Pts',(-1.54118963552779,0.553614476292706,
-3.50791814852041));
#31395=CARTESIAN_POINT('Ctrl Pts',(-1.60738332573138,-0.331738430311634,
-3.46714639909406));
#31396=CARTESIAN_POINT('Ctrl Pts',(-1.2015636321068,-1.12400675283059,-3.42628185077074));
#31397=CARTESIAN_POINT('Ctrl Pts',(-0.440570504989179,-1.58916985286069,
-3.38531848879486));
#31398=CARTESIAN_POINT('Ctrl Pts',(0.454033404816424,-1.5902877858928,-3.34425700144878));
#31399=CARTESIAN_POINT('Ctrl Pts',(1.15461602494958,-1.16119312150655,-3.30653178058679));
#31400=CARTESIAN_POINT('Ctrl Pts',(1.53440095120327,-0.530368167453922,
-3.27216645108545));
#31401=CARTESIAN_POINT('Ctrl Pts',(1.62139701755051,0.127469077736369,-3.24118754526318));
#31402=CARTESIAN_POINT('Ctrl Pts',(1.4375012114545,0.766409474357195,-3.21015627916876));
#31403=CARTESIAN_POINT('Ctrl Pts',(1.01287850477676,1.27928217401078,-3.17907466398971));
#31404=CARTESIAN_POINT('Ctrl Pts',(0.417585531284891,1.58009332728318,-3.14794269660965));
#31405=CARTESIAN_POINT('Ctrl Pts',(-0.24937400777572,1.61780796260654,-3.11676146483555));
#31406=CARTESIAN_POINT('Ctrl Pts',(-0.876750747439923,1.38534894722237,
-3.08553114835378));
#31407=CARTESIAN_POINT('Ctrl Pts',(-1.3596198640501,0.920645586859557,-3.05425345678686));
#31408=CARTESIAN_POINT('Ctrl Pts',(-1.61669866354154,0.300811039804161,
-3.0229270383574));
#31409=CARTESIAN_POINT('Ctrl Pts',(-1.60467642728968,-0.37137754361641,
-2.99155741605365));
#31410=CARTESIAN_POINT('Ctrl Pts',(-1.32404618183457,-0.982979421915755,
-2.96013498111486));
#31411=CARTESIAN_POINT('Ctrl Pts',(-0.766355189816308,-1.48322023143898,
-2.92517889171936));
#31412=CARTESIAN_POINT('Ctrl Pts',(0.0464056028336514,-1.69056552793571,
-2.88665889726854));
#31413=CARTESIAN_POINT('Ctrl Pts',(0.776600509199771,-1.46615811326241,
-2.85157844149717));
#31414=CARTESIAN_POINT('Ctrl Pts',(1.22735642696635,-1.07750731629039,-2.82347612838631));
#31415=CARTESIAN_POINT('Ctrl Pts',(1.47484842707153,-0.705728194344337,
-2.80237963780291));
#31416=CARTESIAN_POINT('Ctrl Pts',(1.61187698899787,-0.280233965655355,
-2.78126552591687));
#31417=CARTESIAN_POINT('Ctrl Pts',(1.63552656943133,0.316004400180914,-2.75308837711847));
#31418=CARTESIAN_POINT('Ctrl Pts',(1.35542815699613,1.03097669758719,-2.71783039275668));
#31419=CARTESIAN_POINT('Ctrl Pts',(0.681591813741207,1.54267081583712,-2.67896420633375));
#31420=CARTESIAN_POINT('Ctrl Pts',(-0.0657304674736995,1.66938144289853,
-2.64361972146493));
#31421=CARTESIAN_POINT('Ctrl Pts',(-0.728459598467511,1.50597117974898,
-2.61169604658853));
#31422=CARTESIAN_POINT('Ctrl Pts',(-1.27108164157649,1.09009694581586,-2.5798958762368));
#31423=CARTESIAN_POINT('Ctrl Pts',(-1.60263472112972,0.491587080445162,
-2.5477443377726));
#31424=CARTESIAN_POINT('Ctrl Pts',(-1.66730050026108,-0.190309275946086,
-2.51615578492575));
#31425=CARTESIAN_POINT('Ctrl Pts',(-1.4535316170482,-0.841935362299378,
-2.48345101010048));
#31426=CARTESIAN_POINT('Ctrl Pts',(-0.99697781119108,-1.35401375496871,
-2.45246871933706));
#31427=CARTESIAN_POINT('Ctrl Pts',(-0.502281440075284,-1.58146609712131,
-2.42602723665317));
#31428=CARTESIAN_POINT('Ctrl Pts',(-0.113329985518638,-1.63932913604753,
-2.40679514213764));
#31429=CARTESIAN_POINT('Ctrl Pts',(0.223307236973708,-1.637305094972,-2.39342050361475));
#31430=CARTESIAN_POINT('Ctrl Pts',(0.803850375083042,-1.49798534345799,
-2.3762688644909));
#31431=CARTESIAN_POINT('Ctrl Pts',(1.48000174465472,-0.929188506823542,
-2.34648398480332));
#31432=CARTESIAN_POINT('Ctrl Pts',(1.74598338432573,0.099297463661904,-2.31347001378341));
#31433=CARTESIAN_POINT('Ctrl Pts',(1.36789648672402,1.09184682624234,-2.27922670008243));
#31434=CARTESIAN_POINT('Ctrl Pts',(0.483572804326568,1.68418169796343,-2.24551390979881));
#31435=CARTESIAN_POINT('Ctrl Pts',(-0.402469297378992,1.65792813194365,
-2.21718495505266));
#31436=CARTESIAN_POINT('Ctrl Pts',(-1.00627030119693,1.33568637362211,-2.19457630535992));
#31437=CARTESIAN_POINT('Ctrl Pts',(-1.36531073202229,0.964891234942623,
-2.17758876089345));
#31438=CARTESIAN_POINT('Ctrl Pts',(-1.59412943474217,0.507099713140616,
-2.16064102435677));
#31439=CARTESIAN_POINT('Ctrl Pts',(-1.64646343907663,0.171569527018422,
-2.14927588835418));
#31440=CARTESIAN_POINT('Ctrl Pts',(-1.64708558907132,-0.00121662450613402,
-2.14365216018176));
#31441=CARTESIAN_POINT('Ctrl Pts',(1.36564437383322,0.00299830309728786,
-4.46698500844523));
#31442=CARTESIAN_POINT('Ctrl Pts',(1.36512056166741,0.14847365365975,-4.46225017397578));
#31443=CARTESIAN_POINT('Ctrl Pts',(1.32205588817515,0.424821325024859,-4.4528904930609));
#31444=CARTESIAN_POINT('Ctrl Pts',(1.13146568593075,0.806300079699337,-4.43876647060324));
#31445=CARTESIAN_POINT('Ctrl Pts',(0.83303740744264,1.11453898701874,-4.42464625577753));
#31446=CARTESIAN_POINT('Ctrl Pts',(0.330622404965623,1.38259481072421,-4.40583938673523));
#31447=CARTESIAN_POINT('Ctrl Pts',(-0.408938205861571,1.4051285585363,-4.38216721772983));
#31448=CARTESIAN_POINT('Ctrl Pts',(-1.14843067370881,0.909838347394963,
-4.35403399920661));
#31449=CARTESIAN_POINT('Ctrl Pts',(-1.4660714086033,0.0779076896382552,
-4.32520462684135));
#31450=CARTESIAN_POINT('Ctrl Pts',(-1.24240261126513,-0.786987507711687,
-4.29770408534344));
#31451=CARTESIAN_POINT('Ctrl Pts',(-0.673251260258778,-1.26651394510792,
-4.27213127287878));
#31452=CARTESIAN_POINT('Ctrl Pts',(-0.112548063135537,-1.40121802635335,
-4.2563114471826));
#31453=CARTESIAN_POINT('Ctrl Pts',(0.433526818334189,-1.36318411131058,
-4.23072532326754));
#31454=CARTESIAN_POINT('Ctrl Pts',(1.02460410701995,-1.04076477994048,-4.19904097395093));
#31455=CARTESIAN_POINT('Ctrl Pts',(1.4205924658604,-0.353935013756109,-4.16290176943614));
#31456=CARTESIAN_POINT('Ctrl Pts',(1.40193814029895,0.373333431475129,-4.12939036340684));
#31457=CARTESIAN_POINT('Ctrl Pts',(1.08535118686797,0.944116541019827,-4.09896301989612));
#31458=CARTESIAN_POINT('Ctrl Pts',(0.618607011932545,1.3019369871989,-4.071507266218));
#31459=CARTESIAN_POINT('Ctrl Pts',(0.0463502533893912,1.44364451385337,
-4.04398496829799));
#31460=CARTESIAN_POINT('Ctrl Pts',(-0.535875961508617,1.34430992342794,
-4.01642164873276));
#31461=CARTESIAN_POINT('Ctrl Pts',(-1.03082420319812,1.01991657951941,-3.98879394504289));
#31462=CARTESIAN_POINT('Ctrl Pts',(-1.35547970359203,0.5236067565516,-3.96111443236515));
#31463=CARTESIAN_POINT('Ctrl Pts',(-1.43810340325584,0.0354024237288245,
-3.93799920689023));
#31464=CARTESIAN_POINT('Ctrl Pts',(-1.38306440274653,-0.351224607303122,
-3.91947818309481));
#31465=CARTESIAN_POINT('Ctrl Pts',(-1.25051960963485,-0.719009372353289,
-3.90093755375014));
#31466=CARTESIAN_POINT('Ctrl Pts',(-0.9478237995269,-1.11338159222678,-3.87772690939149));
#31467=CARTESIAN_POINT('Ctrl Pts',(-0.424254634930679,-1.40256973512589,
-3.84981484028182));
#31468=CARTESIAN_POINT('Ctrl Pts',(0.172150116742664,-1.45812247657558,
-3.82184372666044));
#31469=CARTESIAN_POINT('Ctrl Pts',(0.806355645673129,-1.2500776649494,-3.7906986514273));
#31470=CARTESIAN_POINT('Ctrl Pts',(1.32834851019025,-0.714563943681758,
-3.75635262109906));
#31471=CARTESIAN_POINT('Ctrl Pts',(1.48028559286423,-0.0498447353164157,
-3.72503879231576));
#31472=CARTESIAN_POINT('Ctrl Pts',(1.38038560298628,0.472284190050553,-3.69993305552108));
#31473=CARTESIAN_POINT('Ctrl Pts',(1.14406395494764,0.949230241536377,-3.67479026498734));
#31474=CARTESIAN_POINT('Ctrl Pts',(0.618830831732985,1.39024534500437,-3.64329428001503));
#31475=CARTESIAN_POINT('Ctrl Pts',(-0.197498799202977,1.5136521612102,-3.60538582641974));
#31476=CARTESIAN_POINT('Ctrl Pts',(-0.960858723113836,1.192449871528,-3.5673659492302));
#31477=CARTESIAN_POINT('Ctrl Pts',(-1.44565750094265,0.517835447084338,
-3.52923274996662));
#31478=CARTESIAN_POINT('Ctrl Pts',(-1.50781755081897,-0.312675262246022,
-3.49098527721761));
#31479=CARTESIAN_POINT('Ctrl Pts',(-1.12694040401255,-1.05636654813868,
-3.45262377784345));
#31480=CARTESIAN_POINT('Ctrl Pts',(-0.412229663537864,-1.49333759815456,
-3.4141470035369));
#31481=CARTESIAN_POINT('Ctrl Pts',(0.428529887771001,-1.49443789364399,
-3.37555425331632));
#31482=CARTESIAN_POINT('Ctrl Pts',(1.08747468318201,-1.0909564983591,-3.34007136060003));
#31483=CARTESIAN_POINT('Ctrl Pts',(1.44490170910797,-0.497305657233017,
-3.30772907336355));
#31484=CARTESIAN_POINT('Ctrl Pts',(1.52686081915866,0.122132658888342,-3.27855553874415));
#31485=CARTESIAN_POINT('Ctrl Pts',(1.35362676450459,0.72414602415009,-3.24931620216265));
#31486=CARTESIAN_POINT('Ctrl Pts',(0.953336978464486,1.20768860107748,-3.22001110046922));
#31487=CARTESIAN_POINT('Ctrl Pts',(0.391777207851056,1.49149646372825,-3.19064014526287));
#31488=CARTESIAN_POINT('Ctrl Pts',(-0.237812469329778,1.5271364309313,-3.16120332898548));
#31489=CARTESIAN_POINT('Ctrl Pts',(-0.830452510837174,1.30759332277035,
-3.13170067053968));
#31490=CARTESIAN_POINT('Ctrl Pts',(-1.28691377096919,0.868353783196376,
-3.10213215114974));
#31491=CARTESIAN_POINT('Ctrl Pts',(-1.5301383889915,0.282059188023131,-3.07249793743809));
#31492=CARTESIAN_POINT('Ctrl Pts',(-1.51878600906589,-0.354268344444937,
-3.04279785637424));
#31493=CARTESIAN_POINT('Ctrl Pts',(-1.2530203435885,-0.93363236576551,-3.01303256849989));
#31494=CARTESIAN_POINT('Ctrl Pts',(-0.724301057338272,-1.40791234860284,
-2.97988677408191));
#31495=CARTESIAN_POINT('Ctrl Pts',(0.0468746538144823,-1.60479660643063,
-2.94333378242155));
#31496=CARTESIAN_POINT('Ctrl Pts',(0.740522856114257,-1.39169559570181,
-2.91000702535252));
#31497=CARTESIAN_POINT('Ctrl Pts',(1.16907313648626,-1.02223809055501,-2.8832883223016));
#31498=CARTESIAN_POINT('Ctrl Pts',(1.40448788238127,-0.668614463283503,
-2.86322030241676));
#31499=CARTESIAN_POINT('Ctrl Pts',(1.53492200943615,-0.263670870959058,
-2.84312433060443));
#31500=CARTESIAN_POINT('Ctrl Pts',(1.5574480684303,0.304104721328589,-2.81628922451734));
#31501=CARTESIAN_POINT('Ctrl Pts',(1.29062037388942,0.985613785912805,-2.78268149268605));
#31502=CARTESIAN_POINT('Ctrl Pts',(0.647699213853048,1.47393931268053,-2.74559209089865));
#31503=CARTESIAN_POINT('Ctrl Pts',(-0.0661637106574882,1.59508465851339,
-2.71182558541953));
#31504=CARTESIAN_POINT('Ctrl Pts',(-0.699830879117748,1.43887216823776,
-2.6812977430018));
#31505=CARTESIAN_POINT('Ctrl Pts',(-1.21911543936887,1.04100749299459,-2.6508681567748));
#31506=CARTESIAN_POINT('Ctrl Pts',(-1.53673793949955,0.46767973597802,-2.62006378969118));
#31507=CARTESIAN_POINT('Ctrl Pts',(-1.59885321468961,-0.186031386396118,
-2.58977995398835));
#31508=CARTESIAN_POINT('Ctrl Pts',(-1.39361588679409,-0.811583371395079,
-2.55837730926266));
#31509=CARTESIAN_POINT('Ctrl Pts',(-0.955435913036199,-1.30328784573889,
-2.52863536138063));
#31510=CARTESIAN_POINT('Ctrl Pts',(-0.479035310509762,-1.52243375827867,
-2.50316549095361));
#31511=CARTESIAN_POINT('Ctrl Pts',(-0.105466661007127,-1.57792184412725,
-2.48469593502962));
#31512=CARTESIAN_POINT('Ctrl Pts',(0.217459005539878,-1.57604331226605,
-2.47186352960145));
#31513=CARTESIAN_POINT('Ctrl Pts',(0.776496300339425,-1.44190782037182,
-2.45534243468637));
#31514=CARTESIAN_POINT('Ctrl Pts',(1.42844800473285,-0.893763424640342,
-2.42662776775306));
#31515=CARTESIAN_POINT('Ctrl Pts',(1.68511325308991,0.0984259617408266,
-2.39477486791059));
#31516=CARTESIAN_POINT('Ctrl Pts',(1.32014717838681,1.05709924001896,-2.36169595100801));
#31517=CARTESIAN_POINT('Ctrl Pts',(0.465222197363385,1.62999898968955,-2.32909774949883));
#31518=CARTESIAN_POINT('Ctrl Pts',(-0.392582646808871,1.60464250160246,
-2.30166701854538));
#31519=CARTESIAN_POINT('Ctrl Pts',(-0.977459806552233,1.29256118969725,
-2.2797668583326));
#31520=CARTESIAN_POINT('Ctrl Pts',(-1.32545625001454,0.933217602319048,
-2.26330236782603));
#31521=CARTESIAN_POINT('Ctrl Pts',(-1.54755282926423,0.48896150639208,-2.24685378788748));
#31522=CARTESIAN_POINT('Ctrl Pts',(-1.59831234300574,0.16375824267838,-2.23583746497264));
#31523=CARTESIAN_POINT('Ctrl Pts',(-1.59891715423784,-0.00421251370866319,
-2.23037046506263));
#31524=CARTESIAN_POINT('Ctrl Pts',(1.33274306951509,-0.00184287455380487,
-4.32188217182298));
#31525=CARTESIAN_POINT('Ctrl Pts',(1.33223133781691,0.140277436973989,-4.31725653492141));
#31526=CARTESIAN_POINT('Ctrl Pts',(1.2902720722241,0.409427197339747,-4.30814026546043));
#31527=CARTESIAN_POINT('Ctrl Pts',(1.10439696536374,0.78136050470156,-4.2943679341584));
#31528=CARTESIAN_POINT('Ctrl Pts',(0.813997842438886,1.08124532814599,-4.2806288618531));
#31529=CARTESIAN_POINT('Ctrl Pts',(0.325605208045794,1.34174117966905,-4.2623478198052));
#31530=CARTESIAN_POINT('Ctrl Pts',(-0.392266597046393,1.36343903424653,
-4.23936657717402));
#31531=CARTESIAN_POINT('Ctrl Pts',(-1.10832345882422,0.883510559025349,
-4.21212017602054));
#31532=CARTESIAN_POINT('Ctrl Pts',(-1.41486627333154,0.0794127438512151,
-4.18425457896408));
#31533=CARTESIAN_POINT('Ctrl Pts',(-1.19925904010042,-0.754482629518558,
-4.15773774905943));
#31534=CARTESIAN_POINT('Ctrl Pts',(-0.650749262275713,-1.21597342884471,
-4.13311264221038));
#31535=CARTESIAN_POINT('Ctrl Pts',(-0.112464476894189,-1.3451927619508,
-4.11791636030752));
#31536=CARTESIAN_POINT('Ctrl Pts',(0.408485467307824,-1.30883153454265,
-4.0934966575388));
#31537=CARTESIAN_POINT('Ctrl Pts',(0.97640470620415,-0.999499127010158,
-4.06306058338671));
#31538=CARTESIAN_POINT('Ctrl Pts',(1.35371346551323,-0.343351752449513,
-4.02856921698522));
#31539=CARTESIAN_POINT('Ctrl Pts',(1.33608077413191,0.349832021978961,-3.99661215349609));
#31540=CARTESIAN_POINT('Ctrl Pts',(1.03474305668921,0.892501702089117,-3.9676835930086));
#31541=CARTESIAN_POINT('Ctrl Pts',(0.591711345291201,1.23208009188755,-3.94161859350766));
#31542=CARTESIAN_POINT('Ctrl Pts',(0.0494704427508984,1.36622525558619,
-3.91554324711629));
#31543=CARTESIAN_POINT('Ctrl Pts',(-0.501185464467529,1.27217962308601,
-3.88947074773056));
#31544=CARTESIAN_POINT('Ctrl Pts',(-0.968441061163108,0.965813607757558,
-3.86338487895064));
#31545=CARTESIAN_POINT('Ctrl Pts',(-1.27435653987324,0.497981225383389,
-3.83729470829645));
#31546=CARTESIAN_POINT('Ctrl Pts',(-1.35202798814577,0.0385876101327993,
-3.81554266612973));
#31547=CARTESIAN_POINT('Ctrl Pts',(-1.3002933910548,-0.324722717286434,
-3.79813785235368));
#31548=CARTESIAN_POINT('Ctrl Pts',(-1.17582795675783,-0.670043044415297,
-3.78072900484704));
#31549=CARTESIAN_POINT('Ctrl Pts',(-0.89187979869532,-1.03986513675978,
-3.75895910935149));
#31550=CARTESIAN_POINT('Ctrl Pts',(-0.401602327156241,-1.31055280712498,
-3.73282284913628));
#31551=CARTESIAN_POINT('Ctrl Pts',(0.155958366856248,-1.36240893590434,
-3.70667247880376));
#31552=CARTESIAN_POINT('Ctrl Pts',(0.747921537864027,-1.16810540292178,
-3.67759847337626));
#31553=CARTESIAN_POINT('Ctrl Pts',(1.23417588205323,-0.66901461612135,-3.64559460713661));
#31554=CARTESIAN_POINT('Ctrl Pts',(1.37530120465285,-0.0508038734447465,
-3.61647247222503));
#31555=CARTESIAN_POINT('Ctrl Pts',(1.28250774044461,0.434054084292527,-3.59315698123624));
#31556=CARTESIAN_POINT('Ctrl Pts',(1.06322527327332,0.876535608048439,-3.56983009646951));
#31557=CARTESIAN_POINT('Ctrl Pts',(0.576461744420599,1.28506020436211,-3.54064402683342));
#31558=CARTESIAN_POINT('Ctrl Pts',(-0.17856418654777,1.39900778239141,-3.50558326489951));
#31559=CARTESIAN_POINT('Ctrl Pts',(-0.883333366011173,1.10227489402814,
-3.47047628213641));
#31560=CARTESIAN_POINT('Ctrl Pts',(-1.33009571946298,0.480304216542129,
-3.43532259018841));
#31561=CARTESIAN_POINT('Ctrl Pts',(-1.3871497940757,-0.284071969407902,
-3.400120449005));
#31562=CARTESIAN_POINT('Ctrl Pts',(-1.03698097164857,-0.967464807651622,
-3.36486363385704));
#31563=CARTESIAN_POINT('Ctrl Pts',(-0.381019254282027,-1.36835922625891,
-3.3295520402089));
#31564=CARTESIAN_POINT('Ctrl Pts',(0.389481902092793,-1.36921541021497,
-3.29418330968172));
#31565=CARTESIAN_POINT('Ctrl Pts',(0.99252740309322,-0.999836303890874,
-3.26170597024635));
#31566=CARTESIAN_POINT('Ctrl Pts',(1.31925718593453,-0.457044062570797,
-3.23213556718674));
#31567=CARTESIAN_POINT('Ctrl Pts',(1.39408265408951,0.108809587769026,-3.20548497542942));
#31568=CARTESIAN_POINT('Ctrl Pts',(1.23592254623773,0.658265411917513,-3.17879700908046));
#31569=CARTESIAN_POINT('Ctrl Pts',(0.870829270178407,1.09922483787908,-3.1520701953278));
#31570=CARTESIAN_POINT('Ctrl Pts',(0.3590595432658,1.35782293568119,-3.1253036554442));
#31571=CARTESIAN_POINT('Ctrl Pts',(-0.214278054221324,1.39023954473062,
-3.09849630861867));
#31572=CARTESIAN_POINT('Ctrl Pts',(-0.753588776103895,1.19041365958991,
-3.07164723768404));
#31573=CARTESIAN_POINT('Ctrl Pts',(-1.16869614334255,0.79091857588073,-3.04475523338839));
#31574=CARTESIAN_POINT('Ctrl Pts',(-1.38973889931854,0.258015243465068,
-3.0178197887389));
#31575=CARTESIAN_POINT('Ctrl Pts',(-1.37939392416049,-0.320037143804488,
-2.99083883865735));
#31576=CARTESIAN_POINT('Ctrl Pts',(-1.13807569240459,-0.846049140219926,
-2.96381384874762));
#31577=CARTESIAN_POINT('Ctrl Pts',(-0.658226832417825,-1.27644576592453,
-2.93373256101117));
#31578=CARTESIAN_POINT('Ctrl Pts',(0.0412819538892306,-1.45498650097557,
-2.90057659370659));
#31579=CARTESIAN_POINT('Ctrl Pts',(0.670130684154375,-1.26174671522835,
-2.87036221549118));
#31580=CARTESIAN_POINT('Ctrl Pts',(1.05852260489413,-0.926906152284757,
-2.84614667670633));
#31581=CARTESIAN_POINT('Ctrl Pts',(1.27183260914496,-0.606478431066315,
-2.82796258395378));
#31582=CARTESIAN_POINT('Ctrl Pts',(1.38999725539795,-0.239618169544361,
-2.80975639288988));
#31583=CARTESIAN_POINT('Ctrl Pts',(1.41039635928432,0.274677801973151,-2.78544881465415));
#31584=CARTESIAN_POINT('Ctrl Pts',(1.16873795631116,0.891852165624323,-2.75501303859493));
#31585=CARTESIAN_POINT('Ctrl Pts',(0.586622638095276,1.33397028424145,-2.72143197804221));
#31586=CARTESIAN_POINT('Ctrl Pts',(-0.0596281256868166,1.44364111061832,
-2.69086336929062));
#31587=CARTESIAN_POINT('Ctrl Pts',(-0.633235989998081,1.3022324586094,-2.66322875649725));
#31588=CARTESIAN_POINT('Ctrl Pts',(-1.10328636165357,0.942095047700372,
-2.63568453117449));
#31589=CARTESIAN_POINT('Ctrl Pts',(-1.39079426918394,0.423121775306233,
-2.60780030435273));
#31590=CARTESIAN_POINT('Ctrl Pts',(-1.4470391517022,-0.168622442050105,
-2.5803875186506));
#31591=CARTESIAN_POINT('Ctrl Pts',(-1.26122050903116,-0.734959886532534,
-2.55195681738039));
#31592=CARTESIAN_POINT('Ctrl Pts',(-0.864561437950006,-1.18011215245744,
-2.5250324432996));
#31593=CARTESIAN_POINT('Ctrl Pts',(-0.43303465558965,-1.37863126059473,
-2.50196116010659));
#31594=CARTESIAN_POINT('Ctrl Pts',(-0.0948241190351269,-1.42885069567028,
-2.48524012798101));
#31595=CARTESIAN_POINT('Ctrl Pts',(0.197430191428771,-1.42716228900735,
-2.47362609443607));
#31596=CARTESIAN_POINT('Ctrl Pts',(0.703761336166771,-1.30567723138343,
-2.45866246090041));
#31597=CARTESIAN_POINT('Ctrl Pts',(1.29440166462931,-0.809154737860619,
-2.43264970036145));
#31598=CARTESIAN_POINT('Ctrl Pts',(1.52702131467381,0.0899263703634786,
-2.40378749618235));
#31599=CARTESIAN_POINT('Ctrl Pts',(1.19621045642616,0.958876843822858,-2.37380181641756));
#31600=CARTESIAN_POINT('Ctrl Pts',(0.421100880351963,1.47853570405988,-2.34424608305228));
#31601=CARTESIAN_POINT('Ctrl Pts',(-0.357252438672992,1.45540691718553,
-2.31935534673135));
#31602=CARTESIAN_POINT('Ctrl Pts',(-0.887864026428122,1.17236987553731,
-2.29948793573597));
#31603=CARTESIAN_POINT('Ctrl Pts',(-1.2036269552239,0.846331645317162,-2.2845505972963));
#31604=CARTESIAN_POINT('Ctrl Pts',(-1.40562203409675,0.442258134242617,
-2.26958820164171));
#31605=CARTESIAN_POINT('Ctrl Pts',(-1.45149398156005,0.148118824010667,
-2.25962526863212));
#31606=CARTESIAN_POINT('Ctrl Pts',(-1.45204722659375,-0.00553074769862531,
-2.25462438506895));
#31607=CARTESIAN_POINT('Ctrl Pts',(1.42546076165175,-0.00530765277766144,
-4.20517133738338));
#31608=CARTESIAN_POINT('Ctrl Pts',(1.42491678471702,0.145767943482143,-4.20025422986036));
#31609=CARTESIAN_POINT('Ctrl Pts',(1.37993316537481,0.434308395373396,-4.19048113022102));
#31610=CARTESIAN_POINT('Ctrl Pts',(1.18155428429257,0.831168970214002,-4.17578689139102));
#31611=CARTESIAN_POINT('Ctrl Pts',(0.871544594210684,1.15127228944573,-4.16112003380017));
#31612=CARTESIAN_POINT('Ctrl Pts',(0.350551640194094,1.42916686330045,-4.14161998154656));
#31613=CARTESIAN_POINT('Ctrl Pts',(-0.413792109055743,1.45192144808262,
-4.11715319952602));
#31614=CARTESIAN_POINT('Ctrl Pts',(-1.17508330496538,0.941562236530219,
-4.08818474624585));
#31615=CARTESIAN_POINT('Ctrl Pts',(-1.49995829515209,0.0880210153638399,
-4.05861391303029));
#31616=CARTESIAN_POINT('Ctrl Pts',(-1.27166052210779,-0.795183444245264,
-4.03052951567407));
#31617=CARTESIAN_POINT('Ctrl Pts',(-0.690950520898828,-1.28317112464393,
-4.00448330152644));
#31618=CARTESIAN_POINT('Ctrl Pts',(-0.12294966963944,-1.41942987376945,
-3.98844212011088));
#31619=CARTESIAN_POINT('Ctrl Pts',(0.423496713647097,-1.38120666781861,
-3.96281661468422));
#31620=CARTESIAN_POINT('Ctrl Pts',(1.02300739912064,-1.0551451702216,-3.9307007006121));
#31621=CARTESIAN_POINT('Ctrl Pts',(1.41823975399121,-0.366076115830013,
-3.89451447899854));
#31622=CARTESIAN_POINT('Ctrl Pts',(1.39991931769537,0.360157039366418,-3.86102140976031));
#31623=CARTESIAN_POINT('Ctrl Pts',(1.08467609641392,0.927204409436556,-3.83079718639467));
#31624=CARTESIAN_POINT('Ctrl Pts',(0.622524980372356,1.28135687324873,-3.80360683546856));
#31625=CARTESIAN_POINT('Ctrl Pts',(0.0578874714694361,1.42090945106581,
-3.77645990760956));
#31626=CARTESIAN_POINT('Ctrl Pts',(-0.514223733569828,1.32307218876302,
-3.74937178821944));
#31627=CARTESIAN_POINT('Ctrl Pts',(-0.998714825490126,1.00527734669232,
-3.72232273145444));
#31628=CARTESIAN_POINT('Ctrl Pts',(-1.31519899241595,0.521043028789481,
-3.69532359157212));
#31629=CARTESIAN_POINT('Ctrl Pts',(-1.39531790201036,0.0465799073644213,
-3.67286064065657));
#31630=CARTESIAN_POINT('Ctrl Pts',(-1.34194411349281,-0.328091257034254,
-3.65491191111958));
#31631=CARTESIAN_POINT('Ctrl Pts',(-1.21369685084282,-0.683847300971654,
-3.63697744151664));
#31632=CARTESIAN_POINT('Ctrl Pts',(-0.921567460626822,-1.06416207336965,
-3.61458827224222));
#31633=CARTESIAN_POINT('Ctrl Pts',(-0.418267744270508,-1.34190400597337,
-3.58776279660469));
#31634=CARTESIAN_POINT('Ctrl Pts',(0.15284737168046,-1.3948923755348,-3.56097876688141));
#31635=CARTESIAN_POINT('Ctrl Pts',(0.75787751918564,-1.19616425763182,-3.53126429261728));
#31636=CARTESIAN_POINT('Ctrl Pts',(1.25347090588685,-0.68706525974854,-3.49863334111184));
#31637=CARTESIAN_POINT('Ctrl Pts',(1.39673252181696,-0.0584515547948913,
-3.46902548289891));
#31638=CARTESIAN_POINT('Ctrl Pts',(1.30253079349664,0.433452665070667,-3.44537162448077));
#31639=CARTESIAN_POINT('Ctrl Pts',(1.0803141186864,0.881753903034802,-3.42173818773312));
#31640=CARTESIAN_POINT('Ctrl Pts',(0.588097359665638,1.29451734211856,-3.39223897795944));
#31641=CARTESIAN_POINT('Ctrl Pts',(-0.173086256812962,1.40909830299405,
-3.35689534844021));
#31642=CARTESIAN_POINT('Ctrl Pts',(-0.881357490838906,1.11054942131824,
-3.32161122380991));
#31643=CARTESIAN_POINT('Ctrl Pts',(-1.32886706643363,0.487006580167841,
-3.28638134377501));
#31644=CARTESIAN_POINT('Ctrl Pts',(-1.38557808334009,-0.276926493197428,
-3.25120173340727));
#31645=CARTESIAN_POINT('Ctrl Pts',(-1.0363882630001,-0.957761324549181,
-3.21607364568651));
#31646=CARTESIAN_POINT('Ctrl Pts',(-0.384470557285378,-1.35581423463875,
-3.1809910035834));
#31647=CARTESIAN_POINT('Ctrl Pts',(0.378931861892865,-1.35637916104331,
-3.14595073219316));
#31648=CARTESIAN_POINT('Ctrl Pts',(0.974522766535925,-0.991220571877725,
-3.11386844951284));
#31649=CARTESIAN_POINT('Ctrl Pts',(1.29639097284273,-0.456264431544534,
-3.08472938251996));
#31650=CARTESIAN_POINT('Ctrl Pts',(1.36984281760244,0.100180562872646,-3.05852510329464));
#31651=CARTESIAN_POINT('Ctrl Pts',(1.21453148877589,0.639300308820662,-3.03233905402033));
#31652=CARTESIAN_POINT('Ctrl Pts',(0.856945441307693,1.07099928129219,-3.00617072299088));
#31653=CARTESIAN_POINT('Ctrl Pts',(0.356833095406517,1.32357019965779,-2.98001846012586));
#31654=CARTESIAN_POINT('Ctrl Pts',(-0.202218051140845,1.35505852042893,
-2.95388132800849));
#31655=CARTESIAN_POINT('Ctrl Pts',(-0.726946582754659,1.16050631432679,
-2.9277577739672));
#31656=CARTESIAN_POINT('Ctrl Pts',(-1.1299465441325,0.772502868173686,-2.90164700667616));
#31657=CARTESIAN_POINT('Ctrl Pts',(-1.34403191669268,0.256050785853187,
-2.87554684471141));
#31658=CARTESIAN_POINT('Ctrl Pts',(-1.33391812362185,-0.302943109300097,
-2.84945805333028));
#31659=CARTESIAN_POINT('Ctrl Pts',(-1.10089417653263,-0.810576208385297,
-2.8233749691623));
#31660=CARTESIAN_POINT('Ctrl Pts',(-0.638648401405453,-1.22503333555387,
-2.79440524878434));
#31661=CARTESIAN_POINT('Ctrl Pts',(0.0336164314160058,-1.39634316396761,
-2.76254512756927));
#31662=CARTESIAN_POINT('Ctrl Pts',(0.636267885288322,-1.21093971964553,
-2.73358845246346));
#31663=CARTESIAN_POINT('Ctrl Pts',(1.007759880785,-0.890596006587549,-2.71042533758501));
#31664=CARTESIAN_POINT('Ctrl Pts',(1.21153412552955,-0.584442304946323,
-2.69305317374889));
#31665=CARTESIAN_POINT('Ctrl Pts',(1.32424962304316,-0.234381274375833,
-2.67568185871626));
#31666=CARTESIAN_POINT('Ctrl Pts',(1.3436530953898,0.255742201160696,-2.65251890713377));
#31667=CARTESIAN_POINT('Ctrl Pts',(1.11357546301131,0.842698179974569,-2.62357045989763));
#31668=CARTESIAN_POINT('Ctrl Pts',(0.561090606358497,1.26205310456025,-2.59170793150652));
#31669=CARTESIAN_POINT('Ctrl Pts',(-0.0508352331085539,1.36575328346632,
-2.56276540366945));
#31670=CARTESIAN_POINT('Ctrl Pts',(-0.592973398636511,1.23202049926953,
-2.53664894408376));
#31671=CARTESIAN_POINT('Ctrl Pts',(-1.03644162056573,0.892081332980426,
-2.5106568633187));
#31672=CARTESIAN_POINT('Ctrl Pts',(-1.30718685521202,0.403259290541068,
-2.48439821792449));
#31673=CARTESIAN_POINT('Ctrl Pts',(-1.35991594860344,-0.153299990646814,
-2.45861400522989));
#31674=CARTESIAN_POINT('Ctrl Pts',(-1.18555928726333,-0.684735063431868,
-2.43194136639518));
#31675=CARTESIAN_POINT('Ctrl Pts',(-0.8132546917511,-1.10225590690569,-2.40667609365053));
#31676=CARTESIAN_POINT('Ctrl Pts',(-0.410343556007538,-1.28747626481981,
-2.38514102040768));
#31677=CARTESIAN_POINT('Ctrl Pts',(-0.0933128311840905,-1.33466761419352,
-2.36946411351112));
#31678=CARTESIAN_POINT('Ctrl Pts',(0.181125888445284,-1.33299774678052,
-2.35856079586863));
#31679=CARTESIAN_POINT('Ctrl Pts',(0.653791490249138,-1.21955477220406,
-2.34459674189696));
#31680=CARTESIAN_POINT('Ctrl Pts',(1.20414849306589,-0.756529297812768,
-2.32034780120738));
#31681=CARTESIAN_POINT('Ctrl Pts',(1.42067553810763,0.0806085523657789,
-2.29347807537358));
#31682=CARTESIAN_POINT('Ctrl Pts',(1.11285759072241,0.888214135289975,-2.26560569941744));
#31683=CARTESIAN_POINT('Ctrl Pts',(0.393419132618423,1.370470136021,-2.23817723786205));
#31684=CARTESIAN_POINT('Ctrl Pts',(-0.328107222499164,1.34873389309867,
-2.21510443211576));
#31685=CARTESIAN_POINT('Ctrl Pts',(-0.819225865019777,1.08678750638048,
-2.19671571124849));
#31686=CARTESIAN_POINT('Ctrl Pts',(-1.11128135031818,0.785195716061891,
-2.18290075218618));
#31687=CARTESIAN_POINT('Ctrl Pts',(-1.29824655204404,0.41107491982986,-2.16904707212731));
#31688=CARTESIAN_POINT('Ctrl Pts',(-1.3404415250879,0.140232419653471,-2.1598744395522));
#31689=CARTESIAN_POINT('Ctrl Pts',(-1.34095616469068,-0.00269548703267205,
-2.15522251757602));
#31690=CARTESIAN_POINT('Ctrl Pts',(1.57441728237085,-0.00475882175917087,
-4.20555490878314));
#31691=CARTESIAN_POINT('Ctrl Pts',(1.57382104694255,0.160830226396227,-4.20016542712911));
#31692=CARTESIAN_POINT('Ctrl Pts',(1.52389433620377,0.480836487680276,-4.18932537087206));
#31693=CARTESIAN_POINT('Ctrl Pts',(1.30515998157577,0.918375631205172,-4.17312689334584));
#31694=CARTESIAN_POINT('Ctrl Pts',(0.962591725337778,1.27211015243739,-4.15691751004377));
#31695=CARTESIAN_POINT('Ctrl Pts',(0.386859917276029,1.57929111008162,-4.13536808842013));
#31696=CARTESIAN_POINT('Ctrl Pts',(-0.457385721719227,1.60423173067857,
-4.10834473833266));
#31697=CARTESIAN_POINT('Ctrl Pts',(-1.29867867696178,1.04045295771887,-4.07633236307808));
#31698=CARTESIAN_POINT('Ctrl Pts',(-1.65759157297858,0.0972318401616007,
-4.04365867882984));
#31699=CARTESIAN_POINT('Ctrl Pts',(-1.40535915011805,-0.878658956485217,
-4.01262510582776));
#31700=CARTESIAN_POINT('Ctrl Pts',(-0.76365245051989,-1.4178801751674,-3.98384488263533));
#31701=CARTESIAN_POINT('Ctrl Pts',(-0.13609330725123,-1.56840947170582,
-3.96612093503963));
#31702=CARTESIAN_POINT('Ctrl Pts',(0.467361043861925,-1.52619301427989,
-3.93782048116129));
#31703=CARTESIAN_POINT('Ctrl Pts',(1.12965724939298,-1.16599408387728,-3.9023405236412));
#31704=CARTESIAN_POINT('Ctrl Pts',(1.56602152108927,-0.405070446115325,
-3.86238346280934));
#31705=CARTESIAN_POINT('Ctrl Pts',(1.54577900864213,0.396653620287876,-3.82540733153194));
#31706=CARTESIAN_POINT('Ctrl Pts',(1.19784827952487,1.0224148314103,-3.79205256002208));
#31707=CARTESIAN_POINT('Ctrl Pts',(0.687987022616282,1.41310185049113,-3.76205514281994));
#31708=CARTESIAN_POINT('Ctrl Pts',(0.0652988913500439,1.56696985038245,
-3.7321173863171));
#31709=CARTESIAN_POINT('Ctrl Pts',(-0.565374176136498,1.4590868805882,-3.70225538850416));
#31710=CARTESIAN_POINT('Ctrl Pts',(-1.09920151379461,1.10888693229534,-3.67245008645755));
#31711=CARTESIAN_POINT('Ctrl Pts',(-1.44772778366656,0.5755650513305,-3.6427143272373));
#31712=CARTESIAN_POINT('Ctrl Pts',(-1.53588854207107,0.0532839053016955,
-3.61798686327434));
#31713=CARTESIAN_POINT('Ctrl Pts',(-1.47715703636958,-0.358947593017698,
-3.59823839277339));
#31714=CARTESIAN_POINT('Ctrl Pts',(-1.33608585602734,-0.750253882144961,
-3.57851135695625));
#31715=CARTESIAN_POINT('Ctrl Pts',(-1.01486531301105,-1.16838041624213,
-3.55389397218704));
#31716=CARTESIAN_POINT('Ctrl Pts',(-0.461841975369745,-1.47350276179219,
-3.5244185529707));
#31717=CARTESIAN_POINT('Ctrl Pts',(0.165241246410054,-1.53164105217326,
-3.49500902468416));
#31718=CARTESIAN_POINT('Ctrl Pts',(0.829065654552701,-1.31352985004596,
-3.46240462216341));
#31719=CARTESIAN_POINT('Ctrl Pts',(1.37225900810044,-0.75538743290293,-3.4266337605291));
#31720=CARTESIAN_POINT('Ctrl Pts',(1.52901259893303,-0.0670223596449696,
-3.39421187953474));
#31721=CARTESIAN_POINT('Ctrl Pts',(1.42593328942179,0.471128805235677,-3.36833269058636));
#31722=CARTESIAN_POINT('Ctrl Pts',(1.18294681660127,0.96127347508502,-3.34249244595469));
#31723=CARTESIAN_POINT('Ctrl Pts',(0.645152558547863,1.41209702090449,-3.31026398403709));
#31724=CARTESIAN_POINT('Ctrl Pts',(-0.185257230536811,1.53693202566853,
-3.27170662449143));
#31725=CARTESIAN_POINT('Ctrl Pts',(-0.956824533914112,1.21152432946623,
-3.23326407354796));
#31726=CARTESIAN_POINT('Ctrl Pts',(-1.44351220487384,0.533089995718998,
-3.19493637614729));
#31727=CARTESIAN_POINT('Ctrl Pts',(-1.50493990529097,-0.296700747515234,
-3.15672350641668));
#31728=CARTESIAN_POINT('Ctrl Pts',(-1.12605725802962,-1.03499330356064,
-3.11862311978851));
#31729=CARTESIAN_POINT('Ctrl Pts',(-0.420109128147001,-1.46582906237508,
-3.08063579956));
#31730=CARTESIAN_POINT('Ctrl Pts',(0.405019871121438,-1.46621440348742,
-3.04276070099534));
#31731=CARTESIAN_POINT('Ctrl Pts',(1.04753237367876,-1.07208721947632,-3.00814341308827));
#31732=CARTESIAN_POINT('Ctrl Pts',(1.39414809541201,-0.495776795432331,
-2.9767535852974));
#31733=CARTESIAN_POINT('Ctrl Pts',(1.47307655905306,0.102798097369403,-2.94856378184586));
#31734=CARTESIAN_POINT('Ctrl Pts',(1.30615908686342,0.681855117890808,-2.92043510027654));
#31735=CARTESIAN_POINT('Ctrl Pts',(0.922564785236653,1.1448063648757,-2.89236677996251));
#31736=CARTESIAN_POINT('Ctrl Pts',(0.386946304111455,1.41519990400736,-2.86435840991392));
#31737=CARTESIAN_POINT('Ctrl Pts',(-0.210822359191289,1.44876915553345,
-2.83640937479909));
#31738=CARTESIAN_POINT('Ctrl Pts',(-0.770966689462007,1.24097992849669,
-2.80851922712657));
#31739=CARTESIAN_POINT('Ctrl Pts',(-1.20042387811736,0.827353496504227,
-2.78068709373845));
#31740=CARTESIAN_POINT('Ctrl Pts',(-1.42813960270921,0.277769872489742,
-2.75291296719939));
#31741=CARTESIAN_POINT('Ctrl Pts',(-1.41727339448313,-0.316071267297309,
-2.72519479229085));
#31742=CARTESIAN_POINT('Ctrl Pts',(-1.17009004112573,-0.85433932467822,
-2.69753499960645));
#31743=CARTESIAN_POINT('Ctrl Pts',(-0.680601408236679,-1.2930213408344,
-2.66686129038018));
#31744=CARTESIAN_POINT('Ctrl Pts',(0.0296769378175122,-1.4737959396875,
-2.63320025147592));
#31745=CARTESIAN_POINT('Ctrl Pts',(0.664787577307854,-1.2781518322714,-2.60267843039133));
#31746=CARTESIAN_POINT('Ctrl Pts',(1.05557427000303,-0.941121519830643,
-2.57830843402094));
#31747=CARTESIAN_POINT('Ctrl Pts',(1.26965186401621,-0.619418917470924,
-2.56005427954324));
#31748=CARTESIAN_POINT('Ctrl Pts',(1.38790872959175,-0.252058453272585,
-2.54182372891326));
#31749=CARTESIAN_POINT('Ctrl Pts',(1.40818671885242,0.261657220706895,-2.51754455036367));
#31750=CARTESIAN_POINT('Ctrl Pts',(1.16730350603785,0.875619151982967,-2.48725804038439));
#31751=CARTESIAN_POINT('Ctrl Pts',(0.59065049556,1.31296285283833,-2.45401003554107));
#31752=CARTESIAN_POINT('Ctrl Pts',(-0.0464288866481118,1.42080548531835,
-2.42387439318964));
#31753=CARTESIAN_POINT('Ctrl Pts',(-0.609707723834696,1.28173853674385,
-2.39673722570843));
#31754=CARTESIAN_POINT('Ctrl Pts',(-1.06945689724283,0.929144114286014,
-2.36978219725697));
#31755=CARTESIAN_POINT('Ctrl Pts',(-1.34955685669284,0.42327905257989,-2.3426113838214));
#31756=CARTESIAN_POINT('Ctrl Pts',(-1.40380914218791,-0.151670211794406,
-2.31596897050105));
#31757=CARTESIAN_POINT('Ctrl Pts',(-1.22422606355349,-0.699096895131267,
-2.28849786355966));
#31758=CARTESIAN_POINT('Ctrl Pts',(-0.840591520559868,-1.12894210887443,
-2.26246759589968));
#31759=CARTESIAN_POINT('Ctrl Pts',(-0.428235892457692,-1.31834260254916,
-2.24043266848866));
#31760=CARTESIAN_POINT('Ctrl Pts',(-0.102146798812591,-1.36704794478444,
-2.22430320026236));
#31761=CARTESIAN_POINT('Ctrl Pts',(0.180846350600063,-1.36521149131664,
-2.21306317611664));
#31762=CARTESIAN_POINT('Ctrl Pts',(0.664454998342927,-1.2490959498437,-2.19877907084499));
#31763=CARTESIAN_POINT('Ctrl Pts',(1.22624897429462,-0.775934691994764,
-2.17400695093128));
#31764=CARTESIAN_POINT('Ctrl Pts',(1.44687003037503,0.0775045360740113,
-2.14661308652914));
#31765=CARTESIAN_POINT('Ctrl Pts',(1.13340694971711,0.898760021455017,-2.11826252462912));
#31766=CARTESIAN_POINT('Ctrl Pts',(0.403206857004132,1.38786931881886,-2.09042681193968));
#31767=CARTESIAN_POINT('Ctrl Pts',(-0.32737568430479,1.36560820478861,-2.06706160097662));
#31768=CARTESIAN_POINT('Ctrl Pts',(-0.82372998777544,1.10080520427326,-2.04847494658758));
#31769=CARTESIAN_POINT('Ctrl Pts',(-1.11861986291797,0.79623547986047,-2.03452387002307));
#31770=CARTESIAN_POINT('Ctrl Pts',(-1.30704892942855,0.419117638021289,
-2.02055942174402));
#31771=CARTESIAN_POINT('Ctrl Pts',(-1.34962126675225,0.146088642239538,
-2.0113116407006));
#31772=CARTESIAN_POINT('Ctrl Pts',(-1.35013945947752,0.00217394721176147,
-2.00662760139703));
#31773=CARTESIAN_POINT('Ctrl Pts',(1.66767056912729,-0.000642017226719769,
-4.32172504735902));
#31774=CARTESIAN_POINT('Ctrl Pts',(1.66704137074608,0.174101642915884,-4.31603760751327));
#31775=CARTESIAN_POINT('Ctrl Pts',(1.61396148033041,0.513998779793965,-4.30452227032905));
#31776=CARTESIAN_POINT('Ctrl Pts',(1.3823231309458,0.977381813422264,-4.28736816567594));
#31777=CARTESIAN_POINT('Ctrl Pts',(1.0187270628173,1.35287697793601,-4.27016111559797));
#31778=CARTESIAN_POINT('Ctrl Pts',(0.407282097129691,1.67921088591362,-4.2472729970449));
#31779=CARTESIAN_POINT('Ctrl Pts',(-0.490224177097036,1.70583634833358,
-4.21854378626941));
#31780=CARTESIAN_POINT('Ctrl Pts',(-1.38612305014723,1.10583080364825,-4.18445474003016));
#31781=CARTESIAN_POINT('Ctrl Pts',(-1.76918891341576,0.10015298243074,-4.14961437587636));
#31782=CARTESIAN_POINT('Ctrl Pts',(-1.49979119562877,-0.942078102670249,
-4.1164687536911));
#31783=CARTESIAN_POINT('Ctrl Pts',(-0.814195262826672,-1.51872809084673,
-4.08569913393494));
#31784=CARTESIAN_POINT('Ctrl Pts',(-0.142049463935964,-1.68002727973188,
-4.06672107646415));
#31785=CARTESIAN_POINT('Ctrl Pts',(0.507025639203875,-1.63469298371086,
-4.0362894700067));
#31786=CARTESIAN_POINT('Ctrl Pts',(1.21604512412555,-1.24866425143607,-3.99829501018615));
#31787=CARTESIAN_POINT('Ctrl Pts',(1.68579278403846,-0.431030856387725,
-3.955329441603));
#31788=CARTESIAN_POINT('Ctrl Pts',(1.66385557197735,0.431794240343084,-3.91554634111577));
#31789=CARTESIAN_POINT('Ctrl Pts',(1.28907716480298,1.10639395357867,-3.87958490606665));
#31790=CARTESIAN_POINT('Ctrl Pts',(0.738851377208214,1.52806612434031,-3.84721380241475));
#31791=CARTESIAN_POINT('Ctrl Pts',(0.0661622682049421,1.69438919204168,
-3.81486774991119));
#31792=CARTESIAN_POINT('Ctrl Pts',(-0.616052772511665,1.5777818830296,-3.78256539435748));
#31793=CARTESIAN_POINT('Ctrl Pts',(-1.19415530829946,1.19862620912885,-3.7502887861161));
#31794=CARTESIAN_POINT('Ctrl Pts',(-1.57205496953799,0.620518762079344,
-3.71805226111082));
#31795=CARTESIAN_POINT('Ctrl Pts',(-1.66779537720002,0.0537257236388898,
-3.69121580691083));
#31796=CARTESIAN_POINT('Ctrl Pts',(-1.60402429743041,-0.393980244119804,
-3.66976771840974));
#31797=CARTESIAN_POINT('Ctrl Pts',(-1.4507479604018,-0.819179962498136,
-3.64833182858519));
#31798=CARTESIAN_POINT('Ctrl Pts',(-1.10147601660805,-1.27392279763523,
-3.62155991068323));
#31799=CARTESIAN_POINT('Ctrl Pts',(-0.499520414491787,-1.60612504451686,
-3.58947384999649));
#31800=CARTESIAN_POINT('Ctrl Pts',(0.183740564834017,-1.66954417804101,
-3.55742862876955));
#31801=CARTESIAN_POINT('Ctrl Pts',(0.907739575347634,-1.4317423227012,-3.52186870049055));
#31802=CARTESIAN_POINT('Ctrl Pts',(1.50088512449773,-0.822485081018016,
-3.48281468467816));
#31803=CARTESIAN_POINT('Ctrl Pts',(1.67233660105827,-0.0701090324061639,
-3.44737620589621));
#31804=CARTESIAN_POINT('Ctrl Pts',(1.55960131068257,0.518603001360326,-3.41906570333355));
#31805=CARTESIAN_POINT('Ctrl Pts',(1.29367344519901,1.05507798675663,-3.39078305610274));
#31806=CARTESIAN_POINT('Ctrl Pts',(0.70464689250189,1.54900028873722,-3.35547910665054));
#31807=CARTESIAN_POINT('Ctrl Pts',(-0.205850321961123,1.6860000359595,-3.31320221883856));
#31808=CARTESIAN_POINT('Ctrl Pts',(-1.05269691843797,1.32897874669926,-3.27101092652693));
#31809=CARTESIAN_POINT('Ctrl Pts',(-1.58740406658215,0.583802887696571,
-3.2289089373416));
#31810=CARTESIAN_POINT('Ctrl Pts',(-1.65503960428557,-0.328442529779849,
-3.18689851586196));
#31811=CARTESIAN_POINT('Ctrl Pts',(-1.23827554083022,-1.14076816918272,
-3.14498017094276));
#31812=CARTESIAN_POINT('Ctrl Pts',(-0.461083528427763,-1.61518777248162,
-3.10315676474998));
#31813=CARTESIAN_POINT('Ctrl Pts',(0.447958090773294,-1.61569817471631,
-3.06143035596376));
#31814=CARTESIAN_POINT('Ctrl Pts',(1.15625697096653,-1.18129145663195,-3.02327078103035));
#31815=CARTESIAN_POINT('Ctrl Pts',(1.5385483947366,-0.545732429710449,-2.98865340270468));
#31816=CARTESIAN_POINT('Ctrl Pts',(1.62564928333117,0.114622962233726,-2.95755433957182));
#31817=CARTESIAN_POINT('Ctrl Pts',(1.44146873106163,0.75365983619543,-2.92651289356067));
#31818=CARTESIAN_POINT('Ctrl Pts',(1.01804401786004,1.26471542389246,-2.89552948842941));
#31819=CARTESIAN_POINT('Ctrl Pts',(0.426652198015164,1.56328680486315,-2.86460483166852));
#31820=CARTESIAN_POINT('Ctrl Pts',(-0.233506697337365,1.60037716016785,
-2.8337394357706));
#31821=CARTESIAN_POINT('Ctrl Pts',(-0.852223154769246,1.37087508639121,
-2.80293386593878));
#31822=CARTESIAN_POINT('Ctrl Pts',(-1.32665537063582,0.913951584283742,
-2.77218870761467));
#31823=CARTESIAN_POINT('Ctrl Pts',(-1.57824191563113,0.306770803570071,
-2.74150432467094));
#31824=CARTESIAN_POINT('Ctrl Pts',(-1.56625075181747,-0.349333715748526,
-2.71088155852775));
#31825=CARTESIAN_POINT('Ctrl Pts',(-1.29312932697022,-0.944069321172231,
-2.68032007848504));
#31826=CARTESIAN_POINT('Ctrl Pts',(-0.752337350493662,-1.42875332810076,
-2.64643273964627));
#31827=CARTESIAN_POINT('Ctrl Pts',(0.0323708011696732,-1.62844696738958,
-2.60924549419053));
#31828=CARTESIAN_POINT('Ctrl Pts',(0.733911033259907,-1.41233998754078,
-2.57553270735194));
#31829=CARTESIAN_POINT('Ctrl Pts',(1.16549836573762,-1.04010955882194,-2.54861902978767));
#31830=CARTESIAN_POINT('Ctrl Pts',(1.40190416964634,-0.684856361734514,
-2.52846178585523));
#31831=CARTESIAN_POINT('Ctrl Pts',(1.53246914275855,-0.279241252768065,
-2.5083335304625));
#31832=CARTESIAN_POINT('Ctrl Pts',(1.55485929835845,0.287871240875836,-2.48153218805104));
#31833=CARTESIAN_POINT('Ctrl Pts',(1.2889653761743,0.965432901351441,-2.4481085910331));
#31834=CARTESIAN_POINT('Ctrl Pts',(0.65280735996725,1.44787419907493,-2.41143248159939));
#31835=CARTESIAN_POINT('Ctrl Pts',(-0.0496709907156844,1.56673997752695,
-2.37820546358285));
#31836=CARTESIAN_POINT('Ctrl Pts',(-0.670496836366765,1.4134565877183,-2.3482982885944));
#31837=CARTESIAN_POINT('Ctrl Pts',(-1.17699485748593,1.02494445873048,-2.31860068450517));
#31838=CARTESIAN_POINT('Ctrl Pts',(-1.48540922041371,0.467939880309279,
-2.28868623368794));
#31839=CARTESIAN_POINT('Ctrl Pts',(-1.54504707669121,-0.164866028014098,
-2.25936310649287));
#31840=CARTESIAN_POINT('Ctrl Pts',(-1.34758547808486,-0.766865278693161,
-2.22915760524));
#31841=CARTESIAN_POINT('Ctrl Pts',(-0.925619034963152,-1.23950709454415,
-2.20053050227581));
#31842=CARTESIAN_POINT('Ctrl Pts',(-0.47312689178265,-1.44727688910323,
-2.17635467666706));
#31843=CARTESIAN_POINT('Ctrl Pts',(-0.114624145491398,-1.50088266906923,
-2.15862063519408));
#31844=CARTESIAN_POINT('Ctrl Pts',(0.196793771251874,-1.49882011045581,
-2.14625337353289));
#31845=CARTESIAN_POINT('Ctrl Pts',(0.727540895785712,-1.37137349650026,
-2.13057991784179));
#31846=CARTESIAN_POINT('Ctrl Pts',(1.34350840501744,-0.852377020041632,
-2.10341642675301));
#31847=CARTESIAN_POINT('Ctrl Pts',(1.58522614346538,0.0829234946853341,
-2.07339634995277));
#31848=CARTESIAN_POINT('Ctrl Pts',(1.24189990551023,0.982145057415046,-2.04235987875837));
#31849=CARTESIAN_POINT('Ctrl Pts',(0.442964648689932,1.51696223459205,-2.01190849767654));
#31850=CARTESIAN_POINT('Ctrl Pts',(-0.355194757524547,1.49271901522222,
-1.98638599026986));
#31851=CARTESIAN_POINT('Ctrl Pts',(-0.89738743125439,1.20335711287795,-1.96608245344542));
#31852=CARTESIAN_POINT('Ctrl Pts',(-1.21934525660176,0.870788494252831,
-1.95084901288334));
#31853=CARTESIAN_POINT('Ctrl Pts',(-1.42451679199023,0.460127356714556,
-1.93564500481867));
#31854=CARTESIAN_POINT('Ctrl Pts',(-1.47111624563833,0.161276097580042,
-1.92552253081718));
#31855=CARTESIAN_POINT('Ctrl Pts',(-1.47167744855541,0.00541642853791316,
-1.92044971448322));
#31856=CARTESIAN_POINT('Ctrl Pts',(1.63403212256144,0.00396518640864409,
-4.46700040934992));
#31857=CARTESIAN_POINT('Ctrl Pts',(1.633414152876,0.175590365230348,-4.46141446774971));
#31858=CARTESIAN_POINT('Ctrl Pts',(1.58144489680089,0.508631329729613,-4.45013247933363));
#31859=CARTESIAN_POINT('Ctrl Pts',(1.35418050198765,0.963402541592023,-4.43329826263773));
#31860=CARTESIAN_POINT('Ctrl Pts',(0.997092638581031,1.33223572067097,-4.41639895348265));
#31861=CARTESIAN_POINT('Ctrl Pts',(0.396055854287184,1.6530578269441,-4.39389982100857));
#31862=CARTESIAN_POINT('Ctrl Pts',(-0.487453571014309,1.67953391279076,
-4.36562210287137));
#31863=CARTESIAN_POINT('Ctrl Pts',(-1.37107502680974,1.08800919403189,-4.33200538919037));
#31864=CARTESIAN_POINT('Ctrl Pts',(-1.75003909866722,0.0945250095421055,
-4.29758683406486));
#31865=CARTESIAN_POINT('Ctrl Pts',(-1.48325802053995,-0.937337267150294,
-4.26477411104859));
#31866=CARTESIAN_POINT('Ctrl Pts',(-0.804242501024566,-1.50915141701246,
-4.23427743771177));
#31867=CARTESIAN_POINT('Ctrl Pts',(-0.136252735175991,-1.66956614079881,
-4.21542680409255));
#31868=CARTESIAN_POINT('Ctrl Pts',(0.512509777066478,-1.62433935829672,
-4.18502241042396));
#31869=CARTESIAN_POINT('Ctrl Pts',(1.21666653808731,-1.24045434008153,-4.14728096812073));
#31870=CARTESIAN_POINT('Ctrl Pts',(1.68673889866034,-0.42419747492223,-4.1043501154818));
#31871=CARTESIAN_POINT('Ctrl Pts',(1.66463397769277,0.439031814106804,-4.06456655210986));
#31872=CARTESIAN_POINT('Ctrl Pts',(1.28918472074749,1.11554897429905,-4.02850284801316));
#31873=CARTESIAN_POINT('Ctrl Pts',(0.736527490917053,1.53916271070452,-3.99599306584002));
#31874=CARTESIAN_POINT('Ctrl Pts',(0.0597192645547418,1.70665889578166,
-3.96344496434848));
#31875=CARTESIAN_POINT('Ctrl Pts',(-0.62794703823877,1.58923892015398,-3.93088864416245));
#31876=CARTESIAN_POINT('Ctrl Pts',(-1.21173532891019,1.20650455789826,-3.89829917046084));
#31877=CARTESIAN_POINT('Ctrl Pts',(-1.59408295564238,0.621810298139683,
-3.86569345935932));
#31878=CARTESIAN_POINT('Ctrl Pts',(-1.69118658894133,0.0475258757840812,
-3.8385030380821));
#31879=CARTESIAN_POINT('Ctrl Pts',(-1.62649994211147,-0.406741823043796,
-3.81674141081092));
#31880=CARTESIAN_POINT('Ctrl Pts',(-1.47086327230883,-0.838547308822683,
-3.79497317393629));
#31881=CARTESIAN_POINT('Ctrl Pts',(-1.11580800536417,-1.30098277606591,
-3.76775322323976));
#31882=CARTESIAN_POINT('Ctrl Pts',(-0.502727993620926,-1.63947182863287,
-3.73507219388247));
#31883=CARTESIAN_POINT('Ctrl Pts',(0.194426113269872,-1.70429130667039,
-3.70237618329341));
#31884=CARTESIAN_POINT('Ctrl Pts',(0.934459323762974,-1.46137678148219,
-3.66603209917644));
#31885=CARTESIAN_POINT('Ctrl Pts',(1.54212626499169,-0.837565889576726,
-3.62603519928751));
#31886=CARTESIAN_POINT('Ctrl Pts',(1.71836542527733,-0.0653092002937604,
-3.58965833760839));
#31887=CARTESIAN_POINT('Ctrl Pts',(1.60248161771228,0.540059604623297,-3.56054876145131));
#31888=CARTESIAN_POINT('Ctrl Pts',(1.32877336422805,1.09233810609625,-3.53143388939476));
#31889=CARTESIAN_POINT('Ctrl Pts',(0.721562068605517,1.6018082509204,-3.49503283735083));
#31890=CARTESIAN_POINT('Ctrl Pts',(-0.219375445069418,1.74368689460065,
-3.451340537232));
#31891=CARTESIAN_POINT('Ctrl Pts',(-1.09661835982629,1.37415803608944,-3.40764136240512));
#31892=CARTESIAN_POINT('Ctrl Pts',(-1.65190763164543,0.600786199887819,
-3.36393787201356));
#31893=CARTESIAN_POINT('Ctrl Pts',(-1.7225493629562,-0.34824178044434,-3.3202332058754));
#31894=CARTESIAN_POINT('Ctrl Pts',(-1.28828245587157,-1.19528358601106,
-3.27653044626564));
#31895=CARTESIAN_POINT('Ctrl Pts',(-0.476392710097375,-1.69119687112247,
-3.23283283925704));
#31896=CARTESIAN_POINT('Ctrl Pts',(0.475412289608363,-1.69200841214036,
-3.18914326166888));
#31897=CARTESIAN_POINT('Ctrl Pts',(1.21873050036291,-1.23640649976984,-3.14910456666266));
#31898=CARTESIAN_POINT('Ctrl Pts',(1.62068706394748,-0.568391997078336,
-3.11271615020977));
#31899=CARTESIAN_POINT('Ctrl Pts',(1.71248714292806,0.126800675114135,-3.07997564707981));
#31900=CARTESIAN_POINT('Ctrl Pts',(1.51839160569328,0.800623065833593,-3.04724573761884));
#31901=CARTESIAN_POINT('Ctrl Pts',(1.07134132748941,1.34035514363526,-3.01452752981176));
#31902=CARTESIAN_POINT('Ctrl Pts',(0.445952950723967,1.65620521177943,-2.98182242827649));
#31903=CARTESIAN_POINT('Ctrl Pts',(-0.253235621616767,1.69558949724506,
-2.94913153234246));
#31904=CARTESIAN_POINT('Ctrl Pts',(-0.909531081339571,1.45225519765726,
-2.91645625461488));
#31905=CARTESIAN_POINT('Ctrl Pts',(-1.41354765304908,0.966974009737121,
-2.88379759749975));
#31906=CARTESIAN_POINT('Ctrl Pts',(-1.68125974445041,0.321135267881592,
-2.85115727605726));
#31907=CARTESIAN_POINT('Ctrl Pts',(-1.66857814222946,-0.377775811263314,
-2.81853548530576));
#31908=CARTESIAN_POINT('Ctrl Pts',(-1.37733100303391,-1.01221991954475,
-2.78593568804616));
#31909=CARTESIAN_POINT('Ctrl Pts',(-0.799731307240381,-1.53001994492261,
-2.74973597271145));
#31910=CARTESIAN_POINT('Ctrl Pts',(0.0397423073554164,-1.74387296836219,
-2.70995033892348));
#31911=CARTESIAN_POINT('Ctrl Pts',(0.791672052026611,-1.5124223123408,-2.67381718939549));
#31912=CARTESIAN_POINT('Ctrl Pts',(1.2548568142905,-1.11299176670312,-2.6449342586345));
#31913=CARTESIAN_POINT('Ctrl Pts',(1.50878301167248,-0.731448324033336,
-2.62328385326395));
#31914=CARTESIAN_POINT('Ctrl Pts',(1.6491603524909,-0.295437446030695,-2.60164646956971));
#31915=CARTESIAN_POINT('Ctrl Pts',(1.67327475040855,0.314684516226746,-2.57281079466485));
#31916=CARTESIAN_POINT('Ctrl Pts',(1.38702581105008,1.04462363319461,-2.53680591798736));
#31917=CARTESIAN_POINT('Ctrl Pts',(0.700764571894838,1.56526316414046,-2.4972337408036));
#31918=CARTESIAN_POINT('Ctrl Pts',(-0.0581917213931231,1.69379640831307,
-2.4613332982401));
#31919=CARTESIAN_POINT('Ctrl Pts',(-0.729733295442202,1.52804906535047,
-2.42898092007903));
#31920=CARTESIAN_POINT('Ctrl Pts',(-1.2782317500249,1.10745044146276,-2.39682477743175));
#31921=CARTESIAN_POINT('Ctrl Pts',(-1.61261796673324,0.503612684553527,
-2.3643904933464));
#31922=CARTESIAN_POINT('Ctrl Pts',(-1.67745533422548,-0.183031344035318,
-2.33257312444416));
#31923=CARTESIAN_POINT('Ctrl Pts',(-1.46287455872121,-0.837191718445536,
-2.29974535705945));
#31924=CARTESIAN_POINT('Ctrl Pts',(-1.00440147091468,-1.35094671104102,
-2.26863667244565));
#31925=CARTESIAN_POINT('Ctrl Pts',(-0.511166577563946,-1.57752630595462,
-2.24227873605543));
#31926=CARTESIAN_POINT('Ctrl Pts',(-0.121341981681085,-1.63572882933236,
-2.22299746469467));
#31927=CARTESIAN_POINT('Ctrl Pts',(0.216937568381371,-1.63355035713921,
-2.20956133114149));
#31928=CARTESIAN_POINT('Ctrl Pts',(0.795549791365443,-1.49463453149145,
-2.19247015083976));
#31929=CARTESIAN_POINT('Ctrl Pts',(1.46784754973028,-0.928439854007026,
-2.16282908058836));
#31930=CARTESIAN_POINT('Ctrl Pts',(1.73181203384054,0.0928136904787116,
-2.13004544067402));
#31931=CARTESIAN_POINT('Ctrl Pts',(1.35679704380804,1.07578258179391,-2.09612076196744));
#31932=CARTESIAN_POINT('Ctrl Pts',(0.4827459951358,1.6608517766393,-2.06280214834103));
#31933=CARTESIAN_POINT('Ctrl Pts',(-0.39100871803772,1.63458704965102,-2.03486072202743));
#31934=CARTESIAN_POINT('Ctrl Pts',(-0.985173173937378,1.31743448978772,
-2.01261038575294));
#31935=CARTESIAN_POINT('Ctrl Pts',(-1.33815367873876,0.952841687632227,
-1.99590730338613));
#31936=CARTESIAN_POINT('Ctrl Pts',(-1.56280887343282,0.503299446074766,
-1.97926439075081));
#31937=CARTESIAN_POINT('Ctrl Pts',(-1.61417743768913,0.174293206827452,
-1.96811869179015));
#31938=CARTESIAN_POINT('Ctrl Pts',(-1.61478859484591,0.00456003315652596,
-1.96259432990035));
#31939=CARTESIAN_POINT('Ctrl Pts',(1.54486203470619,0.00504105038853388,
-4.50992061443582));
#31940=CARTESIAN_POINT('Ctrl Pts',(1.54427529571177,0.167992708395013,-4.50461697279343));
#31941=CARTESIAN_POINT('Ctrl Pts',(1.4952334965929,0.482267292923238,-4.4939707520506));
#31942=CARTESIAN_POINT('Ctrl Pts',(1.280098125952,0.912812524518765,-4.47803220176687));
#31943=CARTESIAN_POINT('Ctrl Pts',(0.942266254010241,1.26176908060242,-4.46204447315161));
#31944=CARTESIAN_POINT('Ctrl Pts',(0.373481056552319,1.5653533290073,-4.44075200478145));
#31945=CARTESIAN_POINT('Ctrl Pts',(-0.463404247785094,1.59064712143174,
-4.41396463342408));
#31946=CARTESIAN_POINT('Ctrl Pts',(-1.30080065397219,1.03007856052102,-4.38210653434173));
#31947=CARTESIAN_POINT('Ctrl Pts',(-1.66044589527054,0.0879499473794728,
-4.34946171776996));
#31948=CARTESIAN_POINT('Ctrl Pts',(-1.40718897843239,-0.891504108835798,
-4.31831555008915));
#31949=CARTESIAN_POINT('Ctrl Pts',(-0.76257285222428,-1.43463924387864,
-4.28935167453691));
#31950=CARTESIAN_POINT('Ctrl Pts',(-0.127537178656397,-1.58719053169968,
-4.27143387847271));
#31951=CARTESIAN_POINT('Ctrl Pts',(0.490783544164864,-1.54412691424913,
-4.24246133751784));
#31952=CARTESIAN_POINT('Ctrl Pts',(1.16011254877525,-1.17901721909146,-4.20658115748246));
#31953=CARTESIAN_POINT('Ctrl Pts',(1.60839956049189,-0.401427769437864,
-4.16566702807252));
#31954=CARTESIAN_POINT('Ctrl Pts',(1.58726175515024,0.421750876894179,-4.12773560075408));
#31955=CARTESIAN_POINT('Ctrl Pts',(1.22901070732513,1.06761482142423,-4.09330500428777));
#31956=CARTESIAN_POINT('Ctrl Pts',(0.701012634421948,1.4723766837057,-4.06224619965589));
#31957=CARTESIAN_POINT('Ctrl Pts',(0.0538808968029187,1.63260191483167,
-4.03112301381928));
#31958=CARTESIAN_POINT('Ctrl Pts',(-0.604265655641256,1.52029339992018,
-3.99996509335409));
#31959=CARTESIAN_POINT('Ctrl Pts',(-1.16350103648761,1.15373453196215,-3.9687480484786));
#31960=CARTESIAN_POINT('Ctrl Pts',(-1.53013509440704,0.593198427290282,
-3.93748740632736));
#31961=CARTESIAN_POINT('Ctrl Pts',(-1.62337449866167,0.0421151334826504,
-3.91139521879784));
#31962=CARTESIAN_POINT('Ctrl Pts',(-1.56126900627456,-0.39411781117998,
-3.89049778782509));
#31963=CARTESIAN_POINT('Ctrl Pts',(-1.41175571186897,-0.808972539380072,
-3.86958433719094));
#31964=CARTESIAN_POINT('Ctrl Pts',(-1.07045540903568,-1.25359216931913,
-3.8434155366407));
#31965=CARTESIAN_POINT('Ctrl Pts',(-0.480515947183528,-1.57939238134504,
-3.8119666727399));
#31966=CARTESIAN_POINT('Ctrl Pts',(0.19100290161953,-1.64189675622309,-3.78047309491055));
#31967=CARTESIAN_POINT('Ctrl Pts',(0.904540049513209,-1.40777713332295,
-3.74543248330941));
#31968=CARTESIAN_POINT('Ctrl Pts',(1.49121694695292,-0.80572520337984,-3.70682471160733));
#31969=CARTESIAN_POINT('Ctrl Pts',(1.66171129304163,-0.0593325028595491,
-3.67166537676614));
#31970=CARTESIAN_POINT('Ctrl Pts',(1.5496167463837,0.526399295408366,-3.64350147770703));
#31971=CARTESIAN_POINT('Ctrl Pts',(1.28464063960639,1.0611311664764,-3.61531255256961));
#31972=CARTESIAN_POINT('Ctrl Pts',(0.696268858902054,1.55499203424871,-3.58003721182078));
#31973=CARTESIAN_POINT('Ctrl Pts',(-0.216920980436962,1.69287678092493,
-3.53763265470216));
#31974=CARTESIAN_POINT('Ctrl Pts',(-1.06955241283063,1.33391780047904,-3.49516506321254));
#31975=CARTESIAN_POINT('Ctrl Pts',(-1.61014220606482,0.581347239549756,
-3.45263319816296));
#31976=CARTESIAN_POINT('Ctrl Pts',(-1.67917373826321,-0.343620921298622,
-3.41003699377274));
#31977=CARTESIAN_POINT('Ctrl Pts',(-1.25550348658284,-1.17044583037604,
-3.36738575146504));
#31978=CARTESIAN_POINT('Ctrl Pts',(-0.462020640660321,-1.65532153402782,
-3.32467620708539));
#31979=CARTESIAN_POINT('Ctrl Pts',(0.469705448319077,-1.65634021328833,
-3.28191047946903));
#31980=CARTESIAN_POINT('Ctrl Pts',(1.19850015527152,-1.20982487444789,-3.24266160207414));
#31981=CARTESIAN_POINT('Ctrl Pts',(1.59317109062565,-0.554137583148034,
-3.20694338104645));
#31982=CARTESIAN_POINT('Ctrl Pts',(1.68346032775077,0.129027353549663,-3.17477150591299));
#31983=CARTESIAN_POINT('Ctrl Pts',(1.49259046599288,0.791977263040797,-3.14257297314195));
#31984=CARTESIAN_POINT('Ctrl Pts',(1.05233497259996,1.32363786938231,-3.11034993601051));
#31985=CARTESIAN_POINT('Ctrl Pts',(0.435701331628633,1.63516387116315,-3.07810298725901));
#31986=CARTESIAN_POINT('Ctrl Pts',(-0.254528938786086,1.67413199198048,
-3.04583353661053));
#31987=CARTESIAN_POINT('Ctrl Pts',(-0.903190199732295,1.43371965206946,
-3.01354225730577));
#31988=CARTESIAN_POINT('Ctrl Pts',(-1.40196135164732,0.953622409618861,
-2.98123117044023));
#31989=CARTESIAN_POINT('Ctrl Pts',(-1.6672295939013,0.3138788195484,-2.94889948881354));
#31990=CARTESIAN_POINT('Ctrl Pts',(-1.65476459871361,-0.379237401091453,
-2.91655275411879));
#31991=CARTESIAN_POINT('Ctrl Pts',(-1.36561533935134,-1.00925640253928,
-2.88418251158926));
#31992=CARTESIAN_POINT('Ctrl Pts',(-0.791580155685632,-1.52405179134768,
-2.84820516769771));
#31993=CARTESIAN_POINT('Ctrl Pts',(0.0440188697820079,-1.73707316808419,
-2.80860411869647));
#31994=CARTESIAN_POINT('Ctrl Pts',(0.793703939881436,-1.5065313997291,-2.7725852475833));
#31995=CARTESIAN_POINT('Ctrl Pts',(1.25604301727935,-1.10785808168577,-2.74375918621644));
#31996=CARTESIAN_POINT('Ctrl Pts',(1.50972654347214,-0.72674230304296,-2.72213354167433));
#31997=CARTESIAN_POINT('Ctrl Pts',(1.65008105202239,-0.290858305672986,
-2.70050394464286));
#31998=CARTESIAN_POINT('Ctrl Pts',(1.67426371947403,0.31954215732238,-2.67165783625169));
#31999=CARTESIAN_POINT('Ctrl Pts',(1.38767058671888,1.05071135347934,-2.63559821398635));
#32000=CARTESIAN_POINT('Ctrl Pts',(0.699340526719848,1.57321635116522,-2.5959018076405));
#32001=CARTESIAN_POINT('Ctrl Pts',(-0.0630631132721198,1.70239827801748,
-2.5598438057277));
#32002=CARTESIAN_POINT('Ctrl Pts',(-0.738459672332989,1.53580212731004,
-2.52731017136676));
#32003=CARTESIAN_POINT('Ctrl Pts',(-1.29085657604536,1.11232101894069,-2.49493239584644));
#32004=CARTESIAN_POINT('Ctrl Pts',(-1.62801909720545,0.50360740192754,-2.46223591640657));
#32005=CARTESIAN_POINT('Ctrl Pts',(-1.69359681981401,-0.189305516347992,
-2.43013459810603));
#32006=CARTESIAN_POINT('Ctrl Pts',(-1.47670396873442,-0.850502437605762,
-2.39695331495922));
#32007=CARTESIAN_POINT('Ctrl Pts',(-1.01336092382365,-1.36995827385155,
-2.36551397783944));
#32008=CARTESIAN_POINT('Ctrl Pts',(-0.513033351478244,-1.59989730603717,
-2.33877562827901));
#32009=CARTESIAN_POINT('Ctrl Pts',(-0.118638858821434,-1.65866879273177,
-2.3192717897149));
#32010=CARTESIAN_POINT('Ctrl Pts',(0.2231378134643,-1.65654474281072,-2.30569511174964));
#32011=CARTESIAN_POINT('Ctrl Pts',(0.810235746795052,-1.51562520417683,
-2.28835279734094));
#32012=CARTESIAN_POINT('Ctrl Pts',(1.49319309129472,-0.940792787098675,
-2.25825858954862));
#32013=CARTESIAN_POINT('Ctrl Pts',(1.76161999248799,0.0974220507406099,
-2.22493345911928));
#32014=CARTESIAN_POINT('Ctrl Pts',(1.38017223194885,1.09810710677196,-2.19040761292332));
#32015=CARTESIAN_POINT('Ctrl Pts',(0.489443651430728,1.6945190877625,-2.15645393542203));
#32016=CARTESIAN_POINT('Ctrl Pts',(-0.401928537350069,1.66796741397563,
-2.12795487297203));
#32017=CARTESIAN_POINT('Ctrl Pts',(-1.00884755318753,1.34402342569283,-2.10522879430255));
#32018=CARTESIAN_POINT('Ctrl Pts',(-1.36955730416376,0.971469379765492,
-2.08816145749317));
#32019=CARTESIAN_POINT('Ctrl Pts',(-1.59923321977339,0.511901403140453,
-2.07114854304999));
#32020=CARTESIAN_POINT('Ctrl Pts',(-1.65176416971881,0.175099526035226,
-2.05974032540467));
#32021=CARTESIAN_POINT('Ctrl Pts',(-1.65238846619436,0.00171724468601428,
-2.05409719479715));
#32022=CARTESIAN_POINT('Ctrl Pts',(1.49998243058588,0.00487945268456504,
-4.50992061443582));
#32023=CARTESIAN_POINT('Ctrl Pts',(1.49941141170999,0.163465252269264,-4.50475906983506));
#32024=CARTESIAN_POINT('Ctrl Pts',(1.45186405026655,0.468260659554012,-4.49443439156157));
#32025=CARTESIAN_POINT('Ctrl Pts',(1.24285849641208,0.886559230778761,-4.47894878298098));
#32026=CARTESIAN_POINT('Ctrl Pts',(0.914832037666938,1.22538627239788,-4.46342570918691));
#32027=CARTESIAN_POINT('Ctrl Pts',(0.362526476214984,1.52015190223001,-4.44275032349895));
#32028=CARTESIAN_POINT('Ctrl Pts',(-0.450285458827622,1.54477765231458,
-4.41673352060185));
#32029=CARTESIAN_POINT('Ctrl Pts',(-1.26358566414186,1.00029259499041,-4.38579230410963));
#32030=CARTESIAN_POINT('Ctrl Pts',(-1.61297063863451,0.0851696210599042,
-4.35408217822798));
#32031=CARTESIAN_POINT('Ctrl Pts',(-1.36691769149066,-0.86636719535778,
-4.32382427572184));
#32032=CARTESIAN_POINT('Ctrl Pts',(-0.740664712301201,-1.39406711347056,
-4.29568368658589));
#32033=CARTESIAN_POINT('Ctrl Pts',(-0.123568561445898,-1.54231629531191,
-4.27827259231965));
#32034=CARTESIAN_POINT('Ctrl Pts',(0.477570602247783,-1.50045464230821,
-4.25010620760684));
#32035=CARTESIAN_POINT('Ctrl Pts',(1.12799462557692,-1.14561364539286,-4.21523812123688));
#32036=CARTESIAN_POINT('Ctrl Pts',(1.56388513724472,-0.389673012803625,
-4.17546007003578));
#32037=CARTESIAN_POINT('Ctrl Pts',(1.5433188232119,0.410763669941787,-4.13857735821636));
#32038=CARTESIAN_POINT('Ctrl Pts',(1.19490853879333,1.03893941579882,-4.10508910882579));
#32039=CARTESIAN_POINT('Ctrl Pts',(0.681279880783051,1.43269210784687,-4.07487536403218));
#32040=CARTESIAN_POINT('Ctrl Pts',(0.051646821861207,1.58859643745763,-4.04459309324451));
#32041=CARTESIAN_POINT('Ctrl Pts',(-0.588862535961304,1.47930900476985,
-4.01426969238989));
#32042=CARTESIAN_POINT('Ctrl Pts',(-1.13322870809872,1.1225062752352,-3.98388228335323));
#32043=CARTESIAN_POINT('Ctrl Pts',(-1.4902067993283,0.576759659588736,-3.95344539501966));
#32044=CARTESIAN_POINT('Ctrl Pts',(-1.58102020223693,0.0400740757948976,
-3.92803411508518));
#32045=CARTESIAN_POINT('Ctrl Pts',(-1.52052962309553,-0.384828263720139,
-3.90767925424071));
#32046=CARTESIAN_POINT('Ctrl Pts',(-1.3748830928401,-0.788957250234775,
-3.88730621071591));
#32047=CARTESIAN_POINT('Ctrl Pts',(-1.0423371162911,-1.22218867468557,-3.86180720794638));
#32048=CARTESIAN_POINT('Ctrl Pts',(-0.467378790598492,-1.53972799805516,
-3.83115568482052));
#32049=CARTESIAN_POINT('Ctrl Pts',(0.187274531141039,-1.60068158914455,
-3.80045226057647));
#32050=CARTESIAN_POINT('Ctrl Pts',(0.883096272461548,-1.37238382842803,
-3.76628010013367));
#32051=CARTESIAN_POINT('Ctrl Pts',(1.45542862121288,-0.785128737057825,
-3.72861800828645));
#32052=CARTESIAN_POINT('Ctrl Pts',(1.62183852895481,-0.0567398924127903,
-3.69430530328978));
#32053=CARTESIAN_POINT('Ctrl Pts',(1.51242393883133,0.515046269014153,-3.66681113832745));
#32054=CARTESIAN_POINT('Ctrl Pts',(1.25371395215128,1.0371419048164,-3.63928782397711));
#32055=CARTESIAN_POINT('Ctrl Pts',(0.679041108905056,1.51956040430477,-3.60482953394523));
#32056=CARTESIAN_POINT('Ctrl Pts',(-0.213247562120534,1.65433450298338,
-3.56339447382386));
#32057=CARTESIAN_POINT('Ctrl Pts',(-1.04680323812526,1.30346814108,-3.52187569315801));
#32058=CARTESIAN_POINT('Ctrl Pts',(-1.57557751626781,0.567442201034068,
-3.48027478133792));
#32059=CARTESIAN_POINT('Ctrl Pts',(-1.64318830952972,-0.337637019006298,
-3.43859332018342));
#32060=CARTESIAN_POINT('Ctrl Pts',(-1.22844519515377,-1.14714492715669,
-3.39683307764518));
#32061=CARTESIAN_POINT('Ctrl Pts',(-0.451245980735406,-1.62215680765017,
-3.35499576544402));
#32062=CARTESIAN_POINT('Ctrl Pts',(0.461841974941765,-1.62319460304399,
-3.31308315566976));
#32063=CARTESIAN_POINT('Ctrl Pts',(1.17649440309474,-1.18543555842648,-3.27459582000513));
#32064=CARTESIAN_POINT('Ctrl Pts',(1.5636738872075,-0.54221871976191,-3.23955517618414));
#32065=CARTESIAN_POINT('Ctrl Pts',(1.65231581225766,0.128238780519003,-3.20797910267182));
#32066=CARTESIAN_POINT('Ctrl Pts',(1.46493973472583,0.779138006438161,-3.17636441807156));
#32067=CARTESIAN_POINT('Ctrl Pts',(1.03253139188493,1.30136595938992,-3.14471191495533));
#32068=CARTESIAN_POINT('Ctrl Pts',(0.426609970086491,1.60751024918497,-3.11302251069183));
#32069=CARTESIAN_POINT('Ctrl Pts',(-0.251933879032834,1.64584505089144,
-3.08129700553233));
#32070=CARTESIAN_POINT('Ctrl Pts',(-0.889905805470703,1.40942555957253,
-3.04953632759992));
#32071=CARTESIAN_POINT('Ctrl Pts',(-1.38068331350981,0.937053401938582,
-3.01774135131172));
#32072=CARTESIAN_POINT('Ctrl Pts',(-1.64184179716058,0.307317409087506,
-2.98591300518706));
#32073=CARTESIAN_POINT('Ctrl Pts',(-1.62957916709941,-0.37530803509689,
-2.95405221275351));
#32074=CARTESIAN_POINT('Ctrl Pts',(-1.34474730528677,-0.996034495385219,
-2.92215989404433));
#32075=CARTESIAN_POINT('Ctrl Pts',(-0.778879409529726,-1.50350912987896,
-2.88668999089474));
#32076=CARTESIAN_POINT('Ctrl Pts',(0.0452156959044932,-1.71370006437942,
-2.84763094470004));
#32077=CARTESIAN_POINT('Ctrl Pts',(0.785100365893931,-1.486208751186,-2.81208062847635));
#32078=CARTESIAN_POINT('Ctrl Pts',(1.24161679713701,-1.09259013745182,-2.7836165314676));
#32079=CARTESIAN_POINT('Ctrl Pts',(1.49217131201598,-0.716178712962469,
-2.76225639002869));
#32080=CARTESIAN_POINT('Ctrl Pts',(1.63085414425123,-0.285537734548898,
-2.7408855262812));
#32081=CARTESIAN_POINT('Ctrl Pts',(1.65475200752033,0.317728375257333,-2.7123738937245));
#32082=CARTESIAN_POINT('Ctrl Pts',(1.37145521865962,1.04076278423927,-2.67671479060714));
#32083=CARTESIAN_POINT('Ctrl Pts',(0.69041646931577,1.55777895441666,-2.63743464573646));
#32084=CARTESIAN_POINT('Ctrl Pts',(-0.0643948515707663,1.68574777587918,
-2.6017316079884));
#32085=CARTESIAN_POINT('Ctrl Pts',(-0.733422672005601,1.52073388540773,
-2.56950115646222));
#32086=CARTESIAN_POINT('Ctrl Pts',(-1.28085476582717,1.10113604465525,-2.53741554342871));
#32087=CARTESIAN_POINT('Ctrl Pts',(-1.61517951924605,0.4975562304161,-2.50499073603886));
#32088=CARTESIAN_POINT('Ctrl Pts',(-1.68029840248005,-0.189791143389858,
-2.47314557601871));
#32089=CARTESIAN_POINT('Ctrl Pts',(-1.46497737904047,-0.846156793246451,
-2.44020210847229));
#32090=CARTESIAN_POINT('Ctrl Pts',(-1.00508021286665,-1.36188270355857,
-2.40899190246463));
#32091=CARTESIAN_POINT('Ctrl Pts',(-0.507582321376923,-1.59058364540096,
-2.38240038156976));
#32092=CARTESIAN_POINT('Ctrl Pts',(-0.115985349294589,-1.64889286597431,
-2.36303576958252));
#32093=CARTESIAN_POINT('Ctrl Pts',(0.223158570335046,-1.64681924620263,
-2.349562123073));
#32094=CARTESIAN_POINT('Ctrl Pts',(0.806901355148856,-1.50671742388011,
-2.33231544041505));
#32095=CARTESIAN_POINT('Ctrl Pts',(1.48644477626825,-0.934917871941825,
-2.30237235343056));
#32096=CARTESIAN_POINT('Ctrl Pts',(1.75362331696032,0.0983401101520701,
-2.26920259215576));
#32097=CARTESIAN_POINT('Ctrl Pts',(1.37388207698597,1.09486845045221,-2.23481640537456));
#32098=CARTESIAN_POINT('Ctrl Pts',(0.486437491100621,1.68918937268853,-2.20098350021554));
#32099=CARTESIAN_POINT('Ctrl Pts',(-0.402275175720241,1.66276347810902,
-2.172565595614));
#32100=CARTESIAN_POINT('Ctrl Pts',(-1.0075498708897,1.33971834323449,-2.14990060001603));
#32101=CARTESIAN_POINT('Ctrl Pts',(-1.36740441992316,0.968073875003734,
-2.13287342310861));
#32102=CARTESIAN_POINT('Ctrl Pts',(-1.59664060478066,0.509453342147398,
-2.11589441486025));
#32103=CARTESIAN_POINT('Ctrl Pts',(-1.64911395659225,0.173292258411803,
-2.10450673116507));
#32104=CARTESIAN_POINT('Ctrl Pts',(-1.64973702763284,0.000250310089940127,
-2.09887467748946));
#32105=CARTESIAN_POINT('Ctrl Pts',(0.551250187536832,1.40171416652003,-4.45000670703013));
#32106=CARTESIAN_POINT('Ctrl Pts',(0.531806260700359,1.40940188459679,-4.44930721296889));
#32107=CARTESIAN_POINT('Ctrl Pts',(0.221926689463,1.52441165170123,-4.43824995043405));
#32108=CARTESIAN_POINT('Ctrl Pts',(-0.450285458827622,1.54477765231458,
-4.41673352060185));
#32109=CARTESIAN_POINT('Ctrl Pts',(-1.26358566414186,1.00029259499041,-4.38579230410963));
#32110=CARTESIAN_POINT('Ctrl Pts',(-1.61297063863451,0.0851696210599042,
-4.35408217822798));
#32111=CARTESIAN_POINT('Ctrl Pts',(-1.36691769149066,-0.86636719535778,
-4.32382427572184));
#32112=CARTESIAN_POINT('Ctrl Pts',(-0.740664712301201,-1.39406711347056,
-4.29568368658589));
#32113=CARTESIAN_POINT('Ctrl Pts',(-0.123568561445898,-1.54231629531191,
-4.27827259231965));
#32114=CARTESIAN_POINT('Ctrl Pts',(0.477570602247783,-1.50045464230821,
-4.25010620760684));
#32115=CARTESIAN_POINT('Ctrl Pts',(1.12799462557692,-1.14561364539286,-4.21523812123688));
#32116=CARTESIAN_POINT('Ctrl Pts',(1.56388513724472,-0.389673012803625,
-4.17546007003578));
#32117=CARTESIAN_POINT('Ctrl Pts',(1.5433188232119,0.410763669941787,-4.13857735821636));
#32118=CARTESIAN_POINT('Ctrl Pts',(1.19490853879333,1.03893941579882,-4.10508910882579));
#32119=CARTESIAN_POINT('Ctrl Pts',(0.681279880783051,1.43269210784687,-4.07487536403218));
#32120=CARTESIAN_POINT('Ctrl Pts',(0.051646821861207,1.58859643745763,-4.04459309324451));
#32121=CARTESIAN_POINT('Ctrl Pts',(-0.588862535961304,1.47930900476985,
-4.01426969238989));
#32122=CARTESIAN_POINT('Ctrl Pts',(-1.13322870809872,1.1225062752352,-3.98388228335323));
#32123=CARTESIAN_POINT('Ctrl Pts',(-1.4902067993283,0.576759659588736,-3.95344539501966));
#32124=CARTESIAN_POINT('Ctrl Pts',(-1.58102020223693,0.0400740757948976,
-3.92803411508518));
#32125=CARTESIAN_POINT('Ctrl Pts',(-1.52052962309553,-0.384828263720139,
-3.90767925424071));
#32126=CARTESIAN_POINT('Ctrl Pts',(-1.3748830928401,-0.788957250234775,
-3.88730621071591));
#32127=CARTESIAN_POINT('Ctrl Pts',(-1.0423371162911,-1.22218867468557,-3.86180720794638));
#32128=CARTESIAN_POINT('Ctrl Pts',(-0.467378790598492,-1.53972799805516,
-3.83115568482052));
#32129=CARTESIAN_POINT('Ctrl Pts',(0.187274531141039,-1.60068158914455,
-3.80045226057647));
#32130=CARTESIAN_POINT('Ctrl Pts',(0.883096272461548,-1.37238382842803,
-3.76628010013367));
#32131=CARTESIAN_POINT('Ctrl Pts',(1.45542862121288,-0.785128737057825,
-3.72861800828645));
#32132=CARTESIAN_POINT('Ctrl Pts',(1.62183852895481,-0.0567398924127903,
-3.69430530328978));
#32133=CARTESIAN_POINT('Ctrl Pts',(1.51242393883133,0.515046269014153,-3.66681113832745));
#32134=CARTESIAN_POINT('Ctrl Pts',(1.25371395215128,1.0371419048164,-3.63928782397711));
#32135=CARTESIAN_POINT('Ctrl Pts',(0.679041108905056,1.51956040430477,-3.60482953394523));
#32136=CARTESIAN_POINT('Ctrl Pts',(-0.213247562120534,1.65433450298338,
-3.56339447382386));
#32137=CARTESIAN_POINT('Ctrl Pts',(-1.04680323812526,1.30346814108,-3.52187569315801));
#32138=CARTESIAN_POINT('Ctrl Pts',(-1.57557751626781,0.567442201034068,
-3.48027478133792));
#32139=CARTESIAN_POINT('Ctrl Pts',(-1.64318830952972,-0.337637019006298,
-3.43859332018342));
#32140=CARTESIAN_POINT('Ctrl Pts',(-1.22844519515377,-1.14714492715669,
-3.39683307764518));
#32141=CARTESIAN_POINT('Ctrl Pts',(-0.451245980735406,-1.62215680765017,
-3.35499576544402));
#32142=CARTESIAN_POINT('Ctrl Pts',(0.461841974941765,-1.62319460304399,
-3.31308315566976));
#32143=CARTESIAN_POINT('Ctrl Pts',(1.17649440309474,-1.18543555842648,-3.27459582000513));
#32144=CARTESIAN_POINT('Ctrl Pts',(1.5636738872075,-0.54221871976191,-3.23955517618414));
#32145=CARTESIAN_POINT('Ctrl Pts',(1.65231581225766,0.128238780519003,-3.20797910267182));
#32146=CARTESIAN_POINT('Ctrl Pts',(1.46493973472583,0.779138006438161,-3.17636441807156));
#32147=CARTESIAN_POINT('Ctrl Pts',(1.03253139188493,1.30136595938992,-3.14471191495533));
#32148=CARTESIAN_POINT('Ctrl Pts',(0.426609970086491,1.60751024918497,-3.11302251069183));
#32149=CARTESIAN_POINT('Ctrl Pts',(-0.251933879032834,1.64584505089144,
-3.08129700553233));
#32150=CARTESIAN_POINT('Ctrl Pts',(-0.889905805470703,1.40942555957253,
-3.04953632759992));
#32151=CARTESIAN_POINT('Ctrl Pts',(-1.38068331350981,0.937053401938582,
-3.01774135131172));
#32152=CARTESIAN_POINT('Ctrl Pts',(-1.64184179716058,0.307317409087506,
-2.98591300518706));
#32153=CARTESIAN_POINT('Ctrl Pts',(-1.62957916709941,-0.37530803509689,
-2.95405221275351));
#32154=CARTESIAN_POINT('Ctrl Pts',(-1.34474730528677,-0.996034495385219,
-2.92215989404433));
#32155=CARTESIAN_POINT('Ctrl Pts',(-0.778879409529726,-1.50350912987896,
-2.88668999089474));
#32156=CARTESIAN_POINT('Ctrl Pts',(0.0452156959044932,-1.71370006437942,
-2.84763094470004));
#32157=CARTESIAN_POINT('Ctrl Pts',(0.785100365893931,-1.486208751186,-2.81208062847635));
#32158=CARTESIAN_POINT('Ctrl Pts',(1.24161679713701,-1.09259013745182,-2.7836165314676));
#32159=CARTESIAN_POINT('Ctrl Pts',(1.49217131201598,-0.716178712962469,
-2.76225639002869));
#32160=CARTESIAN_POINT('Ctrl Pts',(1.63085414425123,-0.285537734548898,
-2.7408855262812));
#32161=CARTESIAN_POINT('Ctrl Pts',(1.65475200752033,0.317728375257333,-2.7123738937245));
#32162=CARTESIAN_POINT('Ctrl Pts',(1.37145521865962,1.04076278423927,-2.67671479060714));
#32163=CARTESIAN_POINT('Ctrl Pts',(0.69041646931577,1.55777895441666,-2.63743464573646));
#32164=CARTESIAN_POINT('Ctrl Pts',(-0.0643948515707663,1.68574777587918,
-2.6017316079884));
#32165=CARTESIAN_POINT('Ctrl Pts',(-0.733422672005601,1.52073388540773,
-2.56950115646222));
#32166=CARTESIAN_POINT('Ctrl Pts',(-1.28085476582717,1.10113604465525,-2.53741554342871));
#32167=CARTESIAN_POINT('Ctrl Pts',(-1.61517951924605,0.4975562304161,-2.50499073603886));
#32168=CARTESIAN_POINT('Ctrl Pts',(-1.68029840248005,-0.189791143389858,
-2.47314557601871));
#32169=CARTESIAN_POINT('Ctrl Pts',(-1.46497737904047,-0.846156793246451,
-2.44020210847229));
#32170=CARTESIAN_POINT('Ctrl Pts',(-1.00508021286665,-1.36188270355857,
-2.40899190246463));
#32171=CARTESIAN_POINT('Ctrl Pts',(-0.507582321376923,-1.59058364540096,
-2.38240038156976));
#32172=CARTESIAN_POINT('Ctrl Pts',(-0.115985349294589,-1.64889286597431,
-2.36303576958252));
#32173=CARTESIAN_POINT('Ctrl Pts',(0.223158570335046,-1.64681924620263,
-2.349562123073));
#32174=CARTESIAN_POINT('Ctrl Pts',(0.806901355148856,-1.50671742388011,
-2.33231544041505));
#32175=CARTESIAN_POINT('Ctrl Pts',(1.48644477626825,-0.934917871941825,
-2.30237235343056));
#32176=CARTESIAN_POINT('Ctrl Pts',(1.75362331696032,0.0983401101520701,
-2.26920259215576));
#32177=CARTESIAN_POINT('Ctrl Pts',(1.37388207698597,1.09486845045221,-2.23481640537456));
#32178=CARTESIAN_POINT('Ctrl Pts',(0.486437491100621,1.68918937268853,-2.20098350021554));
#32179=CARTESIAN_POINT('Ctrl Pts',(-0.402275175720241,1.66276347810902,
-2.172565595614));
#32180=CARTESIAN_POINT('Ctrl Pts',(-1.0075498708897,1.33971834323449,-2.14990060001603));
#32181=CARTESIAN_POINT('Ctrl Pts',(-1.36740441992316,0.968073875003734,
-2.13287342310861));
#32182=CARTESIAN_POINT('Ctrl Pts',(-1.59664060478066,0.509453342147398,
-2.11589441486025));
#32183=CARTESIAN_POINT('Ctrl Pts',(-1.64911395659225,0.173292258411803,
-2.10450673116507));
#32184=CARTESIAN_POINT('Ctrl Pts',(-1.64973702763284,0.000250310089940127,
-2.09887467748946));
#59165=UNCERTAINTY_MEASURE_WITH_UNIT(LENGTH_MEASURE(0.001),#59205,
'DISTANCE_ACCURACY_VALUE',
'Maximum model space distance between geometric entities at asserted c
onnectivities');
#59182=UNCERTAINTY_MEASURE_WITH_UNIT(LENGTH_MEASURE(0.001),#59205,
'DISTANCE_ACCURACY_VALUE',
'Maximum model space distance between geometric entities at asserted c
onnectivities');
#59187=(
GEOMETRIC_REPRESENTATION_CONTEXT(3)
GLOBAL_UNCERTAINTY_ASSIGNED_CONTEXT((#59165))
GLOBAL_UNIT_ASSIGNED_CONTEXT((#59205,#59207,#59208))
REPRESENTATION_CONTEXT('','3D')
);
#59204=(
GEOMETRIC_REPRESENTATION_CONTEXT(3)
GLOBAL_UNCERTAINTY_ASSIGNED_CONTEXT((#59182))
GLOBAL_UNIT_ASSIGNED_CONTEXT((#59205,#59207,#59208))
REPRESENTATION_CONTEXT('','3D')
);
#59205=(
LENGTH_UNIT()
NAMED_UNIT(*)
SI_UNIT(.CENTI.,.METRE.)
);
#59207=(
NAMED_UNIT(*)
PLANE_ANGLE_UNIT()
SI_UNIT($,.RADIAN.)
);
#59208=(
NAMED_UNIT(*)
SI_UNIT($,.STERADIAN.)
SOLID_ANGLE_UNIT()
);
#59213=SHAPE_DEFINITION_REPRESENTATION(#59234,#59300);
#59234=PRODUCT_DEFINITION_SHAPE('',$,#59322);
#59300=SHAPE_REPRESENTATION('',(#23166),#59187);
#59317=PRODUCT_DEFINITION_CONTEXT('part definition',#59382,'design');
#59322=PRODUCT_DEFINITION('2026-10-23-00-47-20-071',
'11_Block_Hold-Down_Spring_3x33x24.5',#59343,#59317);
#59343=PRODUCT_DEFINITION_FORMATION('',$,#59388);
#59382=APPLICATION_CONTEXT(
'Core Data for Automotive Mechanical Design Process');
#59383=PRODUCT_CONTEXT('part definition',#59382,'mechanical');
#59388=PRODUCT('2026-10-23-00-47-20-071',
'11_Block_Hold-Down_Spring_3x33x24.5',$,(#59383));
#59580=COLOUR_RGB('Grey',0.48,0.52,0.57);
#59581=FILL_AREA_STYLE_COLOUR('',#59580);
#59582=FILL_AREA_STYLE('',(#59581));
#59583=SURFACE_STYLE_FILL_AREA(#59582);
#59584=SURFACE_SIDE_STYLE('',(#59583));
#59585=SURFACE_STYLE_USAGE(.BOTH.,#59584);
#59586=PRESENTATION_STYLE_ASSIGNMENT((#59585));
ENDSEC;
END-ISO-10303-21;
